ISO-10303-21;
HEADER;
FILE_DESCRIPTION (('STEP AP214'),
    '1' );
FILE_NAME ('Snap Open Cable Crossbars 4.step',
    '2026-10-08T22:59:04',
    ( '' ),
    ( '' ),
    'SwSTEP 2.0',
    'SolidWorks 2020',
    '' );
FILE_SCHEMA (( 'AUTOMOTIVE_DESIGN' ));
ENDSEC;

DATA;
#56=COLOUR_RGB ( '', 0.40784314, 0.44705882, 0.49803922) ;
#160=CARTESIAN_POINT ( 'NONE',  ( -16.82055514392394713, 9.950000000011193890, -121.3232019254582497 ) ) ;
#252=ORIENTED_EDGE ( 'NONE', *, *, #113172, .F. ) ;
#528=VECTOR ( 'NONE', #86821, 1000.000000000000000 ) ;
#560=CARTESIAN_POINT ( 'NONE',  ( -17.73285935860190676, 10.85798180380700728, -123.7585618097890148 ) ) ;
#686=CARTESIAN_POINT ( 'NONE',  ( -16.89268316805466341, 9.951721813253341153, -113.1442475214544885 ) ) ;
#704=CARTESIAN_POINT ( 'NONE',  ( -16.86733706339143524, 9.965990529650820662, -121.4031153019987386 ) ) ;
#731=FACE_BOUND ( 'NONE', #81297, .T. ) ;
#741=CYLINDRICAL_SURFACE ( 'NONE', #86628, 0.1999999999999987899 ) ;
#1280=EDGE_CURVE ( 'NONE', #250524, #245594, #200785, .T. ) ;
#1448=CARTESIAN_POINT ( 'NONE',  ( -16.85722902420154767, 9.950000000011135270, -121.2344525262295463 ) ) ;
#1505=EDGE_CURVE ( 'NONE', #78857, #197503, #63577, .T. ) ;
#1570=DIRECTION ( 'NONE',  ( 1.000000000000000000, 0.000000000000000000, 0.000000000000000000 ) ) ;
#1887=AXIS2_PLACEMENT_3D ( 'NONE', #55717, #36223, #236970 ) ;
#1956=EDGE_CURVE ( 'NONE', #221156, #137732, #149255, .T. ) ;
#1976=CARTESIAN_POINT ( 'NONE',  ( 20.09999999999999787, 9.750000000011137757, -109.7500000000000426 ) ) ;
#1985=EDGE_CURVE ( 'NONE', #54629, #150801, #167541, .T. ) ;
#2073=CARTESIAN_POINT ( 'NONE',  ( -16.77683809663752257, 23.65833333334447985, -117.2500000000000284 ) ) ;
#2153=CARTESIAN_POINT ( 'NONE',  ( -16.80469485234341320, 9.942151663152195340, -121.3099668439312495 ) ) ;
#2258=ORIENTED_EDGE ( 'NONE', *, *, #68816, .T. ) ;
#2425=AXIS2_PLACEMENT_3D ( 'NONE', #153513, #135160, #16531 ) ;
#2452=CARTESIAN_POINT ( 'NONE',  ( -18.34374000495060386, 11.47316190337362585, -109.7500000000000284 ) ) ;
#2469=DIRECTION ( 'NONE',  ( 0.000000000000000000, 0.000000000000000000, 1.000000000000000000 ) ) ;
#2490=CARTESIAN_POINT ( 'NONE',  ( -16.94107738177414291, 10.01423928514777373, -121.4500000000000313 ) ) ;
#2663=ORIENTED_EDGE ( 'NONE', *, *, #228153, .T. ) ;
#3281=CARTESIAN_POINT ( 'NONE',  ( -16.86337532320261090, 9.979967204235514089, -121.4489244689828382 ) ) ;
#3374=CARTESIAN_POINT ( 'NONE',  ( -17.04295772865489766, 10.02489942527116362, -121.3500000000000227 ) ) ;
#3597=ORIENTED_EDGE ( 'NONE', *, *, #121516, .T. ) ;
#3620=FACE_OUTER_BOUND ( 'NONE', #218003, .T. ) ;
#3855=LINE ( 'NONE', #162947, #197306 ) ;
#4023=CARTESIAN_POINT ( 'NONE',  ( -16.89935556175728593, 9.950000000011007373, -120.8603236371143765 ) ) ;
#4221=EDGE_LOOP ( 'NONE', ( #8046, #166375, #35510, #225171 ) ) ;
#4244=ORIENTED_EDGE ( 'NONE', *, *, #116881, .T. ) ;
#4583=CARTESIAN_POINT ( 'NONE',  ( 12.29592348164039350, 9.355806591641288250, -116.7911025315462155 ) ) ;
#4759=DIRECTION ( 'NONE',  ( 1.000000000000000000, 0.000000000000000000, 0.000000000000000000 ) ) ;
#4817=ORIENTED_EDGE ( 'NONE', *, *, #228153, .F. ) ;
#5114=AXIS2_PLACEMENT_3D ( 'NONE', #193228, #94104, #74592 ) ;
#5231=ORIENTED_EDGE ( 'NONE', *, *, #65234, .F. ) ;
#5443=DIRECTION ( 'NONE',  ( -1.000000000000000000, 0.000000000000000000, 0.000000000000000000 ) ) ;
#5847=DIRECTION ( 'NONE',  ( -1.000000000000000000, 0.000000000000000000, 0.000000000000000000 ) ) ;
#5933=CARTESIAN_POINT ( 'NONE',  ( -16.89020380669786192, 9.950000000011137047, -113.2574111481105916 ) ) ;
#5947=AXIS2_PLACEMENT_3D ( 'NONE', #243603, #7560, #224027 ) ;
#6035=EDGE_CURVE ( 'NONE', #42531, #162376, #254152, .T. ) ;
#6114=LINE ( 'NONE', #47802, #12499 ) ;
#6185=CARTESIAN_POINT ( 'NONE',  ( -18.40000000000000213, 5.650000000011139001, -113.1500000000000341 ) ) ;
#6257=B_SPLINE_CURVE_WITH_KNOTS ( 'NONE', 3,
 ( #215356, #152863, #193243, #54979, #176266, #94124, #92838, #231100, #214081, #173726 ),
 .UNSPECIFIED., .F., .F.,
 ( 4, 2, 2, 2, 4 ),
 ( 5.273673492279070357E-16, 9.930191194499300776E-05, 0.0001986038238894586325, 0.0003972076477784301329, 0.0007944152955563315004 ),
 .UNSPECIFIED. ) ;
#6435=ORIENTED_EDGE ( 'NONE', *, *, #9915, .F. ) ;
#6696=CARTESIAN_POINT ( 'NONE',  ( -16.90257928357874917, 9.954106821116520010, -113.1362854301137446 ) ) ;
#6832=ORIENTED_EDGE ( 'NONE', *, *, #222160, .T. ) ;
#6909=CARTESIAN_POINT ( 'NONE',  ( 20.99999999999999645, 9.750000000011137757, -113.1500000000000483 ) ) ;
#7153=CARTESIAN_POINT ( 'NONE',  ( 12.25000000000000000, 9.350000000011140955, -117.2500000000000284 ) ) ;
#7166=DIRECTION ( 'NONE',  ( 1.000000000000000000, -0.000000000000000000, -0.000000000000000000 ) ) ;
#7226=CARTESIAN_POINT ( 'NONE',  ( -16.97683809663752186, 9.950000000011138823, -113.9023640181965220 ) ) ;
#7400=EDGE_LOOP ( 'NONE', ( #84665, #242052, #79957, #241776, #151890 ) ) ;
#7560=DIRECTION ( 'NONE',  ( 0.7071067811865493491, 0.7071067811865456854, 0.000000000000000000 ) ) ;
#7568=DIRECTION ( 'NONE',  ( 1.000000000000000000, 1.186688945009010077E-16, 0.000000000000000000 ) ) ;
#7589=CARTESIAN_POINT ( 'NONE',  ( -18.40000000000000213, 11.33174054713631662, -113.1500000000000341 ) ) ;
#7652=AXIS2_PLACEMENT_3D ( 'NONE', #116257, #53697, #91548 ) ;
#7671=PRODUCT_CONTEXT ( 'NONE', #97263, 'mechanical' ) ;
#7792=DIRECTION ( 'NONE',  ( -1.000000000000000000, 1.652117596168391700E-15, 0.000000000000000000 ) ) ;
#8046=ORIENTED_EDGE ( 'NONE', *, *, #97644, .F. ) ;
#8166=ORIENTED_EDGE ( 'NONE', *, *, #252973, .T. ) ;
#8255=DIRECTION ( 'NONE',  ( -1.000000000000000000, 0.000000000000000000, 1.073024830501117725E-15 ) ) ;
#8280=CARTESIAN_POINT ( 'NONE',  ( 18.39999999999999503, 11.47316190337363828, -113.1500000000000341 ) ) ;
#8575=CARTESIAN_POINT ( 'NONE',  ( 18.39999999999999503, 5.650000000011139001, -124.7500000000000426 ) ) ;
#8609=CARTESIAN_POINT ( 'NONE',  ( -16.93860193097148326, 9.993107767340401182, -121.4001383673068801 ) ) ;
#8799=DIRECTION ( 'NONE',  ( -0.5932847527679310229, 0.8049926720990042694, -6.366092712777067056E-16 ) ) ;
#8857=DIRECTION ( 'NONE',  ( -1.186688945009010077E-16, 1.000000000000000000, 0.000000000000000000 ) ) ;
#8906=CARTESIAN_POINT ( 'NONE',  ( -16.27683809663751191, 9.350000000011133849, -109.7500000000000000 ) ) ;
#9312=CARTESIAN_POINT ( 'NONE',  ( -17.11825945287482753, 10.05000000001113847, -113.2500000000000284 ) ) ;
#9915=EDGE_CURVE ( 'NONE', #41586, #55172, #112572, .T. ) ;
#9983=ORIENTED_EDGE ( 'NONE', *, *, #121954, .T. ) ;
#10064=CARTESIAN_POINT ( 'NONE',  ( 15.74999999999999645, 9.350000000011133849, -117.3657431672739762 ) ) ;
#10098=ORIENTED_EDGE ( 'NONE', *, *, #209042, .T. ) ;
#10102=VECTOR ( 'NONE', #232610, 1000.000000000000000 ) ;
#10342=LINE ( 'NONE', #182892, #197938 ) ;
#10372=CARTESIAN_POINT ( 'NONE',  ( -17.29838795458690015, 10.37154985796052920, -111.8952587173832427 ) ) ;
#10414=ORIENTED_EDGE ( 'NONE', *, *, #1280, .F. ) ;
#10586=PLANE ( 'NONE',  #92765 ) ;
#10648=STYLED_ITEM ( 'NONE', ( #72664 ), #85670 ) ;
#10789=DIRECTION ( 'NONE',  ( -0.7071067811865463515, -0.7071067811865487940, 7.587431340288849180E-16 ) ) ;
#10797=CARTESIAN_POINT ( 'NONE',  ( -18.40000000000000213, 11.47316190337364183, -124.6740539331920843 ) ) ;
#11149=AXIS2_PLACEMENT_3D ( 'NONE', #115300, #252237, #114008 ) ;
#11160=CARTESIAN_POINT ( 'NONE',  ( 18.39999999999999147, 8.822561741677553471, -109.7500000000000426 ) ) ;
#11366=DIRECTION ( 'NONE',  ( 0.5932847527679310229, -0.8049926720990042694, 0.000000000000000000 ) ) ;
#11368=AXIS2_PLACEMENT_3D ( 'NONE', #125364, #203609, #121539 ) ;
#11376=FACE_OUTER_BOUND ( 'NONE', #234231, .T. ) ;
#11411=VERTEX_POINT ( 'NONE', #170943 ) ;
#11427=CARTESIAN_POINT ( 'NONE',  ( -18.40000000000000213, 5.650000000011139001, -121.3500000000000369 ) ) ;
#11657=CARTESIAN_POINT ( 'NONE',  ( -17.22767730082994575, 10.34924421247850468, -111.8575713094296162 ) ) ;
#11687=AXIS2_PLACEMENT_3D ( 'NONE', #56431, #193413, #154319 ) ;
#12114=DIRECTION ( 'NONE',  ( 1.000000000000000000, 0.000000000000000000, 0.000000000000000000 ) ) ;
#12146=DIRECTION ( 'NONE',  ( 1.073024830501117725E-15, -0.000000000000000000, -1.000000000000000000 ) ) ;
#12154=ORIENTED_EDGE ( 'NONE', *, *, #175616, .T. ) ;
#12195=CARTESIAN_POINT ( 'NONE',  ( -16.92507428761699018, 9.950000000011140600, -121.2866025403784960 ) ) ;
#12290=CARTESIAN_POINT ( 'NONE',  ( -18.40000000000000213, 11.48667500176882861, -124.7500000000000284 ) ) ;
#12344=CARTESIAN_POINT ( 'NONE',  ( 20.27550659511088682, 9.216043722520002035, -113.1500000000000483 ) ) ;
#12397=ORIENTED_EDGE ( 'NONE', *, *, #45122, .T. ) ;
#12499=VECTOR ( 'NONE', #183493, 1000.000000000000000 ) ;
#12511=CARTESIAN_POINT ( 'NONE',  ( -18.39999999999999858, 11.47867410001043886, -109.7746932163407081 ) ) ;
#12543=AXIS2_PLACEMENT_3D ( 'NONE', #171762, #249987, #174348 ) ;
#12555=CARTESIAN_POINT ( 'NONE',  ( 18.54999999999999716, 8.750000000011182166, -109.7500000000000426 ) ) ;
#12594=CARTESIAN_POINT ( 'NONE',  ( -16.87683809663752399, 9.850000000011144508, -113.9023640181963373 ) ) ;
#12697=ORIENTED_EDGE ( 'NONE', *, *, #183127, .T. ) ;
#12761=DIRECTION ( 'NONE',  ( -1.000000000000000000, 0.000000000000000000, 0.000000000000000000 ) ) ;
#13185=DIRECTION ( 'NONE',  ( -0.000000000000000000, -0.000000000000000000, -1.000000000000000000 ) ) ;
#13396=ORIENTED_EDGE ( 'NONE', *, *, #149417, .T. ) ;
#13775=EDGE_CURVE ( 'NONE', #163086, #37503, #135005, .T. ) ;
#13985=CARTESIAN_POINT ( 'NONE',  ( -16.89318236219976654, 9.951535257886286345, -113.1448703678941854 ) ) ;
#14087=CYLINDRICAL_SURFACE ( 'NONE', #1887, 0.1000000000000001443 ) ;
#14131=EDGE_CURVE ( 'NONE', #11411, #229722, #225463, .T. ) ;
#14167=VERTEX_POINT ( 'NONE', #69005 ) ;
#14209=CARTESIAN_POINT ( 'NONE',  ( 18.39999999999998082, 11.47316190337362585, -109.7500000000000284 ) ) ;
#14422=CARTESIAN_POINT ( 'NONE',  ( -16.79363873026997922, 9.948850229429586634, -121.3461537814455085 ) ) ;
#14519=CARTESIAN_POINT ( 'NONE',  ( -16.94445028196808778, 9.992063609708889516, -113.1073301784184792 ) ) ;
#14870=VERTEX_POINT ( 'NONE', #14519 ) ;
#15155=ORIENTED_EDGE ( 'NONE', *, *, #29871, .T. ) ;
#15206=CARTESIAN_POINT ( 'NONE',  ( -16.87401514999241314, 9.950000000011137047, -113.2199820074682179 ) ) ;
#15217=CARTESIAN_POINT ( 'NONE',  ( 12.60873083341396850, 9.389571634557563939, -118.3176407123691831 ) ) ;
#15255=VERTEX_POINT ( 'NONE', #14209 ) ;
#15275=CARTESIAN_POINT ( 'NONE',  ( -16.85718274719421217, 9.976142314632873820, -113.0633463321825758 ) ) ;
#15512=CARTESIAN_POINT ( 'NONE',  ( -16.91256925476570672, 9.985731158139332209, -113.0323575109947427 ) ) ;
#15710=CARTESIAN_POINT ( 'NONE',  ( -16.77683809663752257, 9.945835743215303282, -121.3360509808958341 ) ) ;
#15728=ORIENTED_EDGE ( 'NONE', *, *, #102361, .F. ) ;
#15869=ORIENTED_EDGE ( 'NONE', *, *, #148852, .T. ) ;
#16310=DIRECTION ( 'NONE',  ( -1.073024830501117725E-15, 0.000000000000000000, 1.000000000000000000 ) ) ;
#16515=DIRECTION ( 'NONE',  ( -1.000000000000000000, -1.646408749285562691E-14, 1.073024830501117725E-15 ) ) ;
#16531=DIRECTION ( 'NONE',  ( 1.000000000000000000, 0.000000000000000000, 0.000000000000000000 ) ) ;
#17099=LINE ( 'NONE', #78316, #114160 ) ;
#17170=DIRECTION ( 'NONE',  ( -1.000000000000000000, 0.000000000000000000, 0.000000000000000000 ) ) ;
#17298=LINE ( 'NONE', #152982, #73068 ) ;
#17346=EDGE_CURVE ( 'NONE', #167339, #26064, #145051, .T. ) ;
#17386=DIRECTION ( 'NONE',  ( 1.073024830501117725E-15, 0.000000000000000000, 1.000000000000000000 ) ) ;
#17445=CARTESIAN_POINT ( 'NONE',  ( -16.87036670365548474, 10.08494996326643189, -121.4500000000000313 ) ) ;
#17566=PLANE ( 'NONE',  #88464 ) ;
#17647=VECTOR ( 'NONE', #199081, 1000.000000000000000 ) ;
#17730=DIRECTION ( 'NONE',  ( -1.000000000000000000, 0.000000000000000000, 0.000000000000000000 ) ) ;
#17906=FACE_OUTER_BOUND ( 'NONE', #86457, .T. ) ;
#18039=DIRECTION ( 'NONE',  ( 0.000000000000000000, 1.000000000000000000, 0.000000000000000000 ) ) ;
#18225=CIRCLE ( 'NONE', #43172, 0.1999999999999987899 ) ;
#18383=PLANE ( 'NONE',  #19577 ) ;
#18416=LINE ( 'NONE', #38012, #231055 ) ;
#19091=VERTEX_POINT ( 'NONE', #250096 ) ;
#19234=CARTESIAN_POINT ( 'NONE',  ( -14.00000000000000178, 9.850000000011133849, -117.2500000000000284 ) ) ;
#19509=CARTESIAN_POINT ( 'NONE',  ( -18.38639463286148867, 11.48019957384713230, -109.7500000000000426 ) ) ;
#19577=AXIS2_PLACEMENT_3D ( 'NONE', #6185, #81842, #236147 ) ;
#19715=CARTESIAN_POINT ( 'NONE',  ( -21.64999999999999858, 10.05000000001113847, -121.3500000000000369 ) ) ;
#19784=CARTESIAN_POINT ( 'NONE',  ( -17.01825945287482966, 10.05000000001113847, -113.1500000000000341 ) ) ;
#19809=CARTESIAN_POINT ( 'NONE',  ( -16.94165728009537375, 9.987869755934930538, -121.3910550085102358 ) ) ;
#20158=CARTESIAN_POINT ( 'NONE',  ( -17.80356949362895236, 10.87673139700259028, -123.7130730242463557 ) ) ;
#20301=CARTESIAN_POINT ( 'NONE',  ( -16.87845715379269507, 9.957858113908168107, -113.1238006510589287 ) ) ;
#20372=CARTESIAN_POINT ( 'NONE',  ( -16.94445028196807002, 9.992063609708893068, -121.3926698215815918 ) ) ;
#20811=CARTESIAN_POINT ( 'NONE',  ( -16.93826681692523550, 10.01142872029886810, -121.4454584673594724 ) ) ;
#21317=CARTESIAN_POINT ( 'NONE',  ( -15.55912972643740488, 8.490870273573721150, -121.3500000000000369 ) ) ;
#21562=ORIENTED_EDGE ( 'NONE', *, *, #164320, .T. ) ;
#21625=ORIENTED_EDGE ( 'NONE', *, *, #89025, .F. ) ;
#21685=ORIENTED_EDGE ( 'NONE', *, *, #147453, .F. ) ;
#21871=VERTEX_POINT ( 'NONE', #19715 ) ;
#22090=CARTESIAN_POINT ( 'NONE',  ( -16.93294127766158752, 10.00328010296601988, -121.4299072658292715 ) ) ;
#22184=PLANE ( 'NONE',  #118190 ) ;
#22337=CARTESIAN_POINT ( 'NONE',  ( -16.84981964351497297, 9.917318234109998798, -121.1303983859805697 ) ) ;
#22470=AXIS2_PLACEMENT_3D ( 'NONE', #222747, #7568, #8857 ) ;
#22728=ORIENTED_EDGE ( 'NONE', *, *, #254760, .T. ) ;
#22776=CARTESIAN_POINT ( 'NONE',  ( 23.24999999999999645, 11.75000000001113953, -121.3500000000000227 ) ) ;
#23216=ORIENTED_EDGE ( 'NONE', *, *, #58608, .T. ) ;
#23241=ORIENTED_EDGE ( 'NONE', *, *, #205482, .F. ) ;
#23800=AXIS2_PLACEMENT_3D ( 'NONE', #98162, #17386, #177764 ) ;
#23907=ORIENTED_EDGE ( 'NONE', *, *, #58608, .F. ) ;
#23999=ORIENTED_EDGE ( 'NONE', *, *, #48663, .T. ) ;
#24255=CARTESIAN_POINT ( 'NONE',  ( -16.89208623190940273, 9.951577948986638944, -121.3552722032183055 ) ) ;
#24755=EDGE_LOOP ( 'NONE', ( #34145, #69048, #197816, #64236 ) ) ;
#24801=CARTESIAN_POINT ( 'NONE',  ( -17.11825945287483108, 9.950000000011124612, -113.1500000000000483 ) ) ;
#24844=CARTESIAN_POINT ( 'NONE',  ( -16.77977881697927032, 9.946601933544062746, -113.1613785731150870 ) ) ;
#25022=CARTESIAN_POINT ( 'NONE',  ( -17.71734398241073905, 10.84235722847571814, -110.7748617469944605 ) ) ;
#25120=EDGE_CURVE ( 'NONE', #106745, #200735, #18225, .T. ) ;
#25179=ORIENTED_EDGE ( 'NONE', *, *, #113169, .T. ) ;
#25279=DIRECTION ( 'NONE',  ( 1.020425574104004196E-15, 1.210927747993693964E-31, -1.000000000000000000 ) ) ;
#25423=VECTOR ( 'NONE', #222179, 1000.000000000000000 ) ;
#25460=EDGE_LOOP ( 'NONE', ( #113551, #53638, #209785, #61153 ) ) ;
#25491=DIRECTION ( 'NONE',  ( -0.000000000000000000, -0.000000000000000000, -1.000000000000000000 ) ) ;
#25493=CARTESIAN_POINT ( 'NONE',  ( -16.85718274719421217, 9.976142314632896912, -121.4366536678175663 ) ) ;
#25576=ORIENTED_EDGE ( 'NONE', *, *, #101765, .T. ) ;
#25841=EDGE_LOOP ( 'NONE', ( #239221, #248234, #73881, #84631, #150600, #82985, #5231, #130720, #93174, #69596, #218813, #61290, #92360, #50469 ) ) ;
#25863=PLANE ( 'NONE',  #22470 ) ;
#25864=ORIENTED_EDGE ( 'NONE', *, *, #97644, .T. ) ;
#26047=TOROIDAL_SURFACE ( 'NONE', #100989, 14.20833333333334103, 0.1000000000000000056 ) ;
#26064=VERTEX_POINT ( 'NONE', #120258 ) ;
#26071=EDGE_CURVE ( 'NONE', #100213, #181223, #65373, .T. ) ;
#26072=CARTESIAN_POINT ( 'NONE',  ( -16.89268316805466341, 9.951721813253341153, -113.1442475214544885 ) ) ;
#26276=CARTESIAN_POINT ( 'NONE',  ( -16.89268316805466341, 9.951721813253341153, -113.1442475214544885 ) ) ;
#26838=CARTESIAN_POINT ( 'NONE',  ( -17.11825945287481687, 10.05000000001113847, -121.3500000000000227 ) ) ;
#26905=CARTESIAN_POINT ( 'NONE',  ( -15.57281606413133979, 9.370655051134635372, -118.0258232559809244 ) ) ;
#26992=UNCERTAINTY_MEASURE_WITH_UNIT (LENGTH_MEASURE( 1.000000000000000082E-05 ), #34825, 'distance_accuracy_value', 'NONE');
#27093=EDGE_LOOP ( 'NONE', ( #59531, #179494, #154095, #92731 ) ) ;
#27164=ORIENTED_EDGE ( 'NONE', *, *, #121516, .F. ) ;
#27283=CARTESIAN_POINT ( 'NONE',  ( -16.87435696428308063, 9.950002462943377424, -113.1499917651666038 ) ) ;
#27312=( BOUNDED_SURFACE ( )  B_SPLINE_SURFACE ( 3, 2, ( 
 ( #135184, #37404, #193907 ),
 ( #39983, #34848, #15275 ),
 ( #153534, #156084, #192614 ),
 ( #234290, #96058, #13985 ) ),
 .UNSPECIFIED., .F., .F., .F. ) 
 B_SPLINE_SURFACE_WITH_KNOTS ( ( 4, 4 ),
 ( 3, 3 ),
 ( 0.0008258556059633777964, 0.0009616864997632737413 ),
 ( 0.000000000000000000, 1.000000000000000000 ),
 .UNSPECIFIED. ) 
 GEOMETRIC_REPRESENTATION_ITEM ( )  RATIONAL_B_SPLINE_SURFACE ( (
 ( 1.000000000000000000, 0.9152888060719349683, 1.000000000000000000),
 ( 1.000000000000000000, 0.9327727094138091868, 1.000000000000000000),
 ( 1.000000000000000000, 0.9369023509258495030, 1.000000000000000000),
 ( 1.000000000000000000, 0.9246339933864486937, 1.000000000000000000) ) ) 
 REPRESENTATION_ITEM ( '' )  SURFACE ( )  );
#27390=ORIENTED_EDGE ( 'NONE', *, *, #207102, .T. ) ;
#27453=VECTOR ( 'NONE', #146351, 1000.000000000000000 ) ;
#27694=DIRECTION ( 'NONE',  ( 0.7071067811865463515, 0.7071067811865487940, 7.587431340288849180E-16 ) ) ;
#27808=VECTOR ( 'NONE', #105968, 1000.000000000000000 ) ;
#27814=LINE ( 'NONE', #229829, #99681 ) ;
#27866=CARTESIAN_POINT ( 'NONE',  ( -15.06774609480955363, 9.417651958852159666, -115.8587873924405045 ) ) ;
#28001=VERTEX_POINT ( 'NONE', #38209 ) ;
#28067=CIRCLE ( 'NONE', #23800, 0.9000000000000014655 ) ;
#28111=CARTESIAN_POINT ( 'NONE',  ( -16.88593481969334320, 9.950560090095466492, -121.3518722569445316 ) ) ;
#28255=AXIS2_PLACEMENT_3D ( 'NONE', #214801, #115711, #209681 ) ;
#28444=CARTESIAN_POINT ( 'NONE',  ( 16.27683809663750125, 9.350000000011137402, -109.7500000000000426 ) ) ;
#28463=( LENGTH_UNIT ( ) NAMED_UNIT ( * ) SI_UNIT ( .MILLI., .METRE. ) );
#28676=ORIENTED_EDGE ( 'NONE', *, *, #133341, .F. ) ;
#29141=EDGE_CURVE ( 'NONE', #75516, #167339, #28067, .T. ) ;
#29299=ORIENTED_EDGE ( 'NONE', *, *, #1505, .F. ) ;
#29321=AXIS2_PLACEMENT_3D ( 'NONE', #126872, #229816, #51152 ) ;
#29389=EDGE_CURVE ( 'NONE', #162352, #180226, #150182, .T. ) ;
#29598=EDGE_CURVE ( 'NONE', #106745, #104724, #17099, .T. ) ;
#29659=( BOUNDED_CURVE ( )  B_SPLINE_CURVE ( 3, ( #36048, #98522, #176849, #55555 ),
 .UNSPECIFIED., .F., .F. ) 
 B_SPLINE_CURVE_WITH_KNOTS ( ( 4, 4 ),
 ( 0.3000847527772393386, 0.5517402753107881752 ),
 .UNSPECIFIED. ) 
 CURVE ( )  GEOMETRIC_REPRESENTATION_ITEM ( )  RATIONAL_B_SPLINE_CURVE ( ( 1.000000000000000000, 0.9947294176030464508, 0.9947294176030464508, 1.000000000000000000 ) ) 
 REPRESENTATION_ITEM ( '' )  );
#29679=FACE_OUTER_BOUND ( 'NONE', #80967, .T. ) ;
#29727=FACE_OUTER_BOUND ( 'NONE', #142125, .T. ) ;
#29775=ORIENTED_EDGE ( 'NONE', *, *, #199738, .F. ) ;
#29871=EDGE_CURVE ( 'NONE', #256969, #250524, #216230, .T. ) ;
#29882=ORIENTED_EDGE ( 'NONE', *, *, #231034, .T. ) ;
#30335=AXIS2_PLACEMENT_3D ( 'NONE', #63901, #143431, #222959 ) ;
#30342=CARTESIAN_POINT ( 'NONE',  ( -18.40000000000000213, 11.75000000001113953, -113.1500000000000341 ) ) ;
#30461=EDGE_CURVE ( 'NONE', #49384, #108024, #147424, .T. ) ;
#30579=DIRECTION ( 'NONE',  ( 0.000000000000000000, 0.000000000000000000, 1.000000000000000000 ) ) ;
#30834=EDGE_CURVE ( 'NONE', #138239, #34950, #150101, .T. ) ;
#31073=PLANE ( 'NONE',  #220928 ) ;
#31398=AXIS2_PLACEMENT_3D ( 'NONE', #234497, #117133, #55835 ) ;
#32075=CARTESIAN_POINT ( 'NONE',  ( -16.93772744219066340, 9.993541108763510650, -113.0980619719697273 ) ) ;
#32111=LINE ( 'NONE', #73811, #168513 ) ;
#32121=FACE_OUTER_BOUND ( 'NONE', #83947, .T. ) ;
#32229=LINE ( 'NONE', #89593, #187035 ) ;
#32524=CARTESIAN_POINT ( 'NONE',  ( -17.27223548804520803, 10.34539739142213222, -111.8663938208072182 ) ) ;
#32551=ORIENTED_EDGE ( 'NONE', *, *, #41269, .F. ) ;
#32622=CARTESIAN_POINT ( 'NONE',  ( -18.39999999999999858, 11.47316190337362762, -109.8259460668080152 ) ) ;
#32687=AXIS2_PLACEMENT_3D ( 'NONE', #6909, #129428, #86416 ) ;
#32847=PRODUCT_DEFINITION_CONTEXT ( 'detailed design', #162437, 'design' ) ;
#32851=CARTESIAN_POINT ( 'NONE',  ( -17.78043020864320667, 10.85359211201684637, -123.6630491657202668 ) ) ;
#33266=AXIS2_PLACEMENT_3D ( 'NONE', #74946, #256059, #154492 ) ;
#33404=VECTOR ( 'NONE', #231245, 1000.000000000000000 ) ;
#33528=CARTESIAN_POINT ( 'NONE',  ( 12.25000000000000178, 9.350000000011140955, -117.3642676076161138 ) ) ;
#33727=VERTEX_POINT ( 'NONE', #26072 ) ;
#33874=B_SPLINE_CURVE_WITH_KNOTS ( 'NONE', 3,
 ( #49187, #10064, #89585, #248679, #90880, #50447, #132587, #149601, #154738, #114297, #135127, #214674, #189991, #253792, #72629, #230396, #36063, #229116, #232987, #51731, #93440, #193847, #15217, #249962, #94729, #231699, #170478, #173038, #33528, #152173 ),
 .UNSPECIFIED., .F., .F.,
 ( 4, 2, 2, 2, 2, 2, 2, 2, 2, 2, 2, 2, 2, 2, 4 ),
 ( 0.000000000000000000, 0.0003422764154113348617, 0.0006845528308226697233, 0.001026829246234006428, 0.001369105661645343350, 0.002053658492468013290, 0.002738211323290683664, 0.003080487738702016465, 0.003422764154113348400, 0.003765040569524680768, 0.004107316984936013569, 0.004449593400347345504, 0.004791869815758678305, 0.005134146231170010240, 0.005476422646581343041 ),
 .UNSPECIFIED. ) ;
#33898=EDGE_CURVE ( 'NONE', #34950, #121961, #211298, .T. ) ;
#34011=DIRECTION ( 'NONE',  ( -0.000000000000000000, 1.000000000000000000, -0.000000000000000000 ) ) ;
#34145=ORIENTED_EDGE ( 'NONE', *, *, #29141, .T. ) ;
#34208=EDGE_CURVE ( 'NONE', #55464, #28001, #165253, .T. ) ;
#34601=VECTOR ( 'NONE', #211664, 1000.000000000000000 ) ;
#34641=CARTESIAN_POINT ( 'NONE',  ( -16.94107738177415712, 10.01423928514777728, -113.0500000000000398 ) ) ;
#34825=( LENGTH_UNIT ( ) NAMED_UNIT ( * ) SI_UNIT ( .MILLI., .METRE. ) );
#34848=CARTESIAN_POINT ( 'NONE',  ( -16.89797118371633999, 9.976380722655555644, -113.0627066324413761 ) ) ;
#34890=CARTESIAN_POINT ( 'NONE',  ( 23.24999999999999645, 8.822561741677553471, -113.1500000000000483 ) ) ;
#34950=VERTEX_POINT ( 'NONE', #138667 ) ;
#34962=CARTESIAN_POINT ( 'NONE',  ( 18.39999999999999503, 5.650000000011139001, -113.1500000000000341 ) ) ;
#35254=AXIS2_PLACEMENT_3D ( 'NONE', #60718, #7166, #144107 ) ;
#35510=ORIENTED_EDGE ( 'NONE', *, *, #210323, .T. ) ;
#35539=CARTESIAN_POINT ( 'NONE',  ( -21.64999999999999858, 10.05000000001113847, -113.1500000000000341 ) ) ;
#35561=CARTESIAN_POINT ( 'NONE',  ( -12.47155713865592297, 9.375669526436929857, -116.3677900093859989 ) ) ;
#35829=ORIENTED_EDGE ( 'NONE', *, *, #253576, .T. ) ;
#35922=CARTESIAN_POINT ( 'NONE',  ( -16.94062896051973865, 9.992719105111833144, -113.1025165421188348 ) ) ;
#36048=CARTESIAN_POINT ( 'NONE',  ( -16.87036670365548474, 9.989418819312801290, -121.4795601173020856 ) ) ;
#36052=CARTESIAN_POINT ( 'NONE',  ( -16.87998658237741978, 9.950000000011073098, -113.3636395677385309 ) ) ;
#36063=CARTESIAN_POINT ( 'NONE',  ( 13.43663047529820709, 9.446645344706402270, -118.9108064561002323 ) ) ;
#36074=CARTESIAN_POINT ( 'NONE',  ( 20.73486653747088226, 7.250000000011182166, -113.1500000000000483 ) ) ;
#36123=CARTESIAN_POINT ( 'NONE',  ( -16.97092634996655036, 10.00088896635952018, -121.3698572337023478 ) ) ;
#36223=DIRECTION ( 'NONE',  ( 0.7071067811865463515, -0.7071067811865487940, 0.000000000000000000 ) ) ;
#36354=CARTESIAN_POINT ( 'NONE',  ( -21.65000000000000213, 9.950000000011140600, -113.1500000000000341 ) ) ;
#36578=CARTESIAN_POINT ( 'NONE',  ( 18.39999999999999503, 5.650000000011139001, -121.3500000000000369 ) ) ;
#36742=PLANE ( 'NONE',  #7652 ) ;
#36820=CARTESIAN_POINT ( 'NONE',  ( -16.94333152882355975, 9.990342011468824168, -121.3920315311015230 ) ) ;
#37302=CARTESIAN_POINT ( 'NONE',  ( -16.86578989773641979, 9.984809801269951990, -113.0353351133777977 ) ) ;
#37381=( NAMED_UNIT ( * ) SI_UNIT ( $, .STERADIAN. ) SOLID_ANGLE_UNIT ( ) );
#37404=CARTESIAN_POINT ( 'NONE',  ( -16.91256925476571027, 9.985731158139330432, -113.0323575109947569 ) ) ;
#37465=CARTESIAN_POINT ( 'NONE',  ( -16.80100914604134132, 9.943149094114721365, -121.3170441272877014 ) ) ;
#37503=VERTEX_POINT ( 'NONE', #65668 ) ;
#37705=VERTEX_POINT ( 'NONE', #95505 ) ;
#38012=CARTESIAN_POINT ( 'NONE',  ( 21.72449340488910252, 10.28395627750227703, -113.1500000000000483 ) ) ;
#38046=CARTESIAN_POINT ( 'NONE',  ( -16.88705144915409306, 9.950000000011199219, -121.0690214052879980 ) ) ;
#38139=CARTESIAN_POINT ( 'NONE',  ( -16.89268316805465986, 9.951721813253337601, -121.3557524785455826 ) ) ;
#38180=ADVANCED_FACE ( 'NONE', ( #212144 ), #227834, .F. ) ;
#38209=CARTESIAN_POINT ( 'NONE',  ( 18.39999999999999503, 11.75000000001113953, -121.3500000000000369 ) ) ;
#38363=VERTEX_POINT ( 'NONE', #20372 ) ;
#38370=CARTESIAN_POINT ( 'NONE',  ( 12.25000000000000000, 9.850000000011137402, -117.2500000000000284 ) ) ;
#38428=CARTESIAN_POINT ( 'NONE',  ( -16.94107738177414291, 10.01423928514777373, -121.4500000000000313 ) ) ;
#38493=ADVANCED_FACE ( 'NONE', ( #54129 ), #17566, .F. ) ;
#38702=CIRCLE ( 'NONE', #30335, 0.5000000000000004441 ) ;
#38926=DIRECTION ( 'NONE',  ( 1.000000000000000000, 0.000000000000000000, 0.000000000000000000 ) ) ;
#38948=CARTESIAN_POINT ( 'NONE',  ( 16.87683809663750267, 9.950000000011138823, -113.1500000000000341 ) ) ;
#39226=CARTESIAN_POINT ( 'NONE',  ( -16.83199030136658081, 9.930648033124622742, -113.2724010226575047 ) ) ;
#39329=CARTESIAN_POINT ( 'NONE',  ( -16.87998658237740912, 9.950000000011137047, -121.1363604322620375 ) ) ;
#39431=ORIENTED_EDGE ( 'NONE', *, *, #230518, .F. ) ;
#39831=CARTESIAN_POINT ( 'NONE',  ( 18.39999999999999503, 11.75000000001113953, -113.1500000000000341 ) ) ;
#39874=CARTESIAN_POINT ( 'NONE',  ( -16.87036670365549895, 9.989418819312803066, -113.0204398826979855 ) ) ;
#39927=ORIENTED_EDGE ( 'NONE', *, *, #144012, .T. ) ;
#39983=CARTESIAN_POINT ( 'NONE',  ( -16.92778301347269121, 10.00094491684630960, -113.0714818920312723 ) ) ;
#40045=VERTEX_POINT ( 'NONE', #252077 ) ;
#40055=EDGE_CURVE ( 'NONE', #221470, #14167, #49075, .T. ) ;
#40450=CARTESIAN_POINT ( 'NONE',  ( 23.04999999999999716, 8.822561741677553471, -124.7500000000000284 ) ) ;
#40632=CARTESIAN_POINT ( 'NONE',  ( -16.77308656112214180, 9.950000000011135270, -121.3498068082977284 ) ) ;
#41028=FACE_OUTER_BOUND ( 'NONE', #216015, .T. ) ;
#41124=CARTESIAN_POINT ( 'NONE',  ( -18.40000000000000213, 11.75000000001113953, -113.1500000000000341 ) ) ;
#41127=ORIENTED_EDGE ( 'NONE', *, *, #60134, .F. ) ;
#41269=EDGE_CURVE ( 'NONE', #150801, #157238, #99759, .T. ) ;
#41586=VERTEX_POINT ( 'NONE', #154053 ) ;
#41805=EDGE_LOOP ( 'NONE', ( #176654, #82304, #164078, #63890 ) ) ;
#41847=CARTESIAN_POINT ( 'NONE',  ( 23.24999999999999645, 5.650000000011139001, -113.1500000000000483 ) ) ;
#42283=AXIS2_PLACEMENT_3D ( 'NONE', #80254, #159850, #17730 ) ;
#42531=VERTEX_POINT ( 'NONE', #124011 ) ;
#42575=CARTESIAN_POINT ( 'NONE',  ( -16.78493211734302903, 9.945835743215326374, -121.3360509808959904 ) ) ;
#42746=AXIS2_PLACEMENT_3D ( 'NONE', #221734, #198345, #163095 ) ;
#42870=CARTESIAN_POINT ( 'NONE',  ( -18.40000000000000213, 11.47316190337362762, -113.0500000000000398 ) ) ;
#43172=AXIS2_PLACEMENT_3D ( 'NONE', #140210, #103649, #198919 ) ;
#43278=ADVANCED_FACE ( 'NONE', ( #185920 ), #189773, .F. ) ;
#43326=FACE_OUTER_BOUND ( 'NONE', #120707, .T. ) ;
#43400=ORIENTED_EDGE ( 'NONE', *, *, #231034, .F. ) ;
#43915=CARTESIAN_POINT ( 'NONE',  ( -23.25000000000000355, 5.650000000011139001, -109.7500000000000426 ) ) ;
#44026=UNCERTAINTY_MEASURE_WITH_UNIT (LENGTH_MEASURE( 1.000000000000000082E-05 ), #28463, 'distance_accuracy_value', 'NONE');
#44113=EDGE_LOOP ( 'NONE', ( #193371, #216421, #105569, #71439, #233970 ) ) ;
#44121=VERTEX_POINT ( 'NONE', #133991 ) ;
#44210=CARTESIAN_POINT ( 'NONE',  ( -18.40000000000000213, 5.650000000011139001, -124.7500000000000426 ) ) ;
#44273=DIRECTION ( 'NONE',  ( 0.000000000000000000, 0.000000000000000000, 1.000000000000000000 ) ) ;
#44569=ORIENTED_EDGE ( 'NONE', *, *, #215736, .T. ) ;
#44971=AXIS2_PLACEMENT_3D ( 'NONE', #76247, #16310, #80067 ) ;
#45012=CARTESIAN_POINT ( 'NONE',  ( 13.12220780326571301, 9.430633469083948839, -115.7317657948240850 ) ) ;
#45122=EDGE_CURVE ( 'NONE', #37503, #250524, #83643, .T. ) ;
#45147=VERTEX_POINT ( 'NONE', #55944 ) ;
#45148=CARTESIAN_POINT ( 'NONE',  ( -14.56336952470180002, 9.446645344706402270, -118.9108064561002323 ) ) ;
#45548=DIRECTION ( 'NONE',  ( 1.000000000000000000, 0.000000000000000000, -0.000000000000000000 ) ) ;
#45680=ORIENTED_EDGE ( 'NONE', *, *, #129978, .T. ) ;
#45800=LINE ( 'NONE', #88755, #133449 ) ;
#45880=PLANE ( 'NONE',  #141550 ) ;
#45986=CARTESIAN_POINT ( 'NONE',  ( 18.39999999999997371, 11.47316190337362940, -124.7500000000000426 ) ) ;
#46173=VERTEX_POINT ( 'NONE', #139461 ) ;
#46206=EDGE_LOOP ( 'NONE', ( #245760, #172074, #234604, #230713, #39431 ) ) ;
#46338=FACE_OUTER_BOUND ( 'NONE', #27093, .T. ) ;
#46419=CARTESIAN_POINT ( 'NONE',  ( -15.31895204843005232, 9.396533993965077158, -118.4059397791733375 ) ) ;
#46588=CARTESIAN_POINT ( 'NONE',  ( 18.39999999999999503, 11.47316190337363828, -124.7500000000000426 ) ) ;
#46625=ADVANCED_FACE ( 'NONE', ( #142989 ), #222531, .F. ) ;
#46837=DIRECTION ( 'NONE',  ( -3.035766082959430717E-14, 0.000000000000000000, -1.000000000000000000 ) ) ;
#46853=FACE_OUTER_BOUND ( 'NONE', #145091, .T. ) ;
#47116=VERTEX_POINT ( 'NONE', #187005 ) ;
#47242=ORIENTED_EDGE ( 'NONE', *, *, #129349, .T. ) ;
#47373=CARTESIAN_POINT ( 'NONE',  ( -15.75000000000001066, 9.350000000011140955, -117.0215193718251072 ) ) ;
#47622=CARTESIAN_POINT ( 'NONE',  ( -16.88328101497759448, 9.950352834230013599, -121.3511795149293135 ) ) ;
#47627=CARTESIAN_POINT ( 'NONE',  ( -16.90137573187933739, 9.950000000011137047, -113.2884174240969344 ) ) ;
#47703=CARTESIAN_POINT ( 'NONE',  ( -15.69373346032659811, 9.356790025057039273, -117.7048265086139480 ) ) ;
#47758=CARTESIAN_POINT ( 'NONE',  ( -18.40000000000000213, 11.75000000001113953, -124.7500000000000284 ) ) ;
#47802=CARTESIAN_POINT ( 'NONE',  ( -16.87683809663752399, 9.850000000011140955, -113.1500000000000341 ) ) ;
#47907=CARTESIAN_POINT ( 'NONE',  ( 20.27550659511088682, 9.216043722520002035, -109.7500000000000426 ) ) ;
#48083=DIRECTION ( 'NONE',  ( 0.000000000000000000, 0.9553114395362780620, -0.2956011730205483912 ) ) ;
#48084=CARTESIAN_POINT ( 'NONE',  ( -16.88815647973234135, 9.950832619326892114, -113.1472170633260390 ) ) ;
#48087=ORIENTED_EDGE ( 'NONE', *, *, #202822, .F. ) ;
#48172=CARTESIAN_POINT ( 'NONE',  ( -16.92209698673559970, 9.950000000011138823, -113.2106355670527478 ) ) ;
#48240=LINE ( 'NONE', #208619, #189860 ) ;
#48550=ORIENTED_EDGE ( 'NONE', *, *, #91439, .T. ) ;
#48663=EDGE_CURVE ( 'NONE', #55464, #135449, #107168, .T. ) ;
#48705=CARTESIAN_POINT ( 'NONE',  ( -18.40000000000000213, 5.650000000011139001, -121.3500000000000369 ) ) ;
#48776=VECTOR ( 'NONE', #175562, 1000.000000000000000 ) ;
#48796=ORIENTED_EDGE ( 'NONE', *, *, #108872, .F. ) ;
#48808=EDGE_LOOP ( 'NONE', ( #207860, #219096, #256968 ) ) ;
#48809=CARTESIAN_POINT ( 'NONE',  ( -16.87683809663752399, 23.65833333334447985, -117.2500000000000284 ) ) ;
#48841=CARTESIAN_POINT ( 'NONE',  ( -18.40000000000000213, 5.650000000011139001, -113.1500000000000341 ) ) ;
#48889=CARTESIAN_POINT ( 'NONE',  ( -16.94878442675511465, 9.991729103002157331, -121.3882195756379048 ) ) ;
#48995=CARTESIAN_POINT ( 'NONE',  ( -12.60829076262180592, 9.389529397477891948, -118.3171079128937322 ) ) ;
#49075=CIRCLE ( 'NONE', #11687, 1.500000000000001332 ) ;
#49092=ORIENTED_EDGE ( 'NONE', *, *, #199738, .T. ) ;
#49187=CARTESIAN_POINT ( 'NONE',  ( 15.74999999999999645, 9.350000000011139178, -117.2500000000000284 ) ) ;
#49316=FACE_OUTER_BOUND ( 'NONE', #237659, .T. ) ;
#49323=CARTESIAN_POINT ( 'NONE',  ( -18.40000000000000213, 11.41458325961095177, -121.3500000000000227 ) ) ;
#49384=VERTEX_POINT ( 'NONE', #38139 ) ;
#49481=FACE_OUTER_BOUND ( 'NONE', #115612, .T. ) ;
#49730=LINE ( 'NONE', #171017, #105155 ) ;
#50203=CARTESIAN_POINT ( 'NONE',  ( -16.94225986326250677, 9.950000000011137047, -113.4467193756079268 ) ) ;
#50447=CARTESIAN_POINT ( 'NONE',  ( 15.57250062127604373, 9.370689921613767126, -118.0264651266610798 ) ) ;
#50469=ORIENTED_EDGE ( 'NONE', *, *, #253576, .F. ) ;
#50597=DIRECTION ( 'NONE',  ( 1.000000000000000000, -0.000000000000000000, -0.000000000000000000 ) ) ;
#50958=DIRECTION ( 'NONE',  ( 0.000000000000000000, -0.000000000000000000, -1.000000000000000000 ) ) ;
#51041=CARTESIAN_POINT ( 'NONE',  ( 15.74999999999999645, 9.850000000011137402, -117.2500000000000284 ) ) ;
#51152=DIRECTION ( 'NONE',  ( -0.7071067811865562325, -0.7071067811865388020, 0.000000000000000000 ) ) ;
#51718=CARTESIAN_POINT ( 'NONE',  ( -16.92280123533722858, 9.950000000011137047, -113.3506323140851464 ) ) ;
#51731=CARTESIAN_POINT ( 'NONE',  ( 12.93279065517212878, 9.417690691074257714, -118.6416006967646410 ) ) ;
#51854=ORIENTED_EDGE ( 'NONE', *, *, #57582, .F. ) ;
#51856=CARTESIAN_POINT ( 'NONE',  ( 22.88900146558018989, 8.703904791123973084, -121.3500000000000227 ) ) ;
#51892=ORIENTED_EDGE ( 'NONE', *, *, #56964, .F. ) ;
#52026=CARTESIAN_POINT ( 'NONE',  ( -17.80356949363855534, 10.87673139701218972, -110.7869269757733548 ) ) ;
#52431=B_SPLINE_CURVE_WITH_KNOTS ( 'NONE', 3,
 ( #244553, #148037, #166346, #47622, #28111, #223697, #146716, #226253, #24255, #107616 ),
 .UNSPECIFIED., .F., .F.,
 ( 4, 3, 3, 4 ),
 ( 0.000000000000000000, 1.004626015991589319E-05, 1.831183478183387304E-05, 2.062343583996250457E-05 ),
 .UNSPECIFIED. ) ;
#52458=VERTEX_POINT ( 'NONE', #243482 ) ;
#52593=CARTESIAN_POINT ( 'NONE',  ( -23.25000000000000355, 5.650000000011139001, -121.3500000000000369 ) ) ;
#52904=ADVANCED_FACE ( 'NONE', ( #46338 ), #26047, .T. ) ;
#52912=VECTOR ( 'NONE', #8799, 1000.000000000000000 ) ;
#53226=DIRECTION ( 'NONE',  ( -0.000000000000000000, -0.000000000000000000, -1.000000000000000000 ) ) ;
#53333=B_SPLINE_CURVE_WITH_KNOTS ( 'NONE', 3,
 ( #246823, #68202, #109876, #10797 ),
 .UNSPECIFIED., .F., .F.,
 ( 4, 4 ),
 ( 0.000000000000000000, 7.713889350926232550E-05 ),
 .UNSPECIFIED. ) ;
#53638=ORIENTED_EDGE ( 'NONE', *, *, #68816, .F. ) ;
#53697=DIRECTION ( 'NONE',  ( -0.7071067811865487940, 0.7071067811865463515, -7.215498431451184074E-16 ) ) ;
#53775=CARTESIAN_POINT ( 'NONE',  ( -16.93935632781549572, 9.984730499736244269, -121.3896607487103410 ) ) ;
#53867=CARTESIAN_POINT ( 'NONE',  ( -17.11825945287481332, 9.950000000011138823, -121.2500000000000426 ) ) ;
#53954=CARTESIAN_POINT ( 'NONE',  ( -18.36973785203556275, 11.47550320049537476, -124.7500000000000284 ) ) ;
#54071=AXIS2_PLACEMENT_3D ( 'NONE', #8575, #89370, #205473 ) ;
#54129=FACE_OUTER_BOUND ( 'NONE', #65812, .T. ) ;
#54375=FACE_OUTER_BOUND ( 'NONE', #219447, .T. ) ;
#54379=CARTESIAN_POINT ( 'NONE',  ( -16.87242674293849021, 9.950000000011138823, -121.3510902463723937 ) ) ;
#54411=CARTESIAN_POINT ( 'NONE',  ( 20.09999999999999787, 9.750000000011137757, -121.3500000000000227 ) ) ;
#54508=FACE_OUTER_BOUND ( 'NONE', #124798, .T. ) ;
#54542=CARTESIAN_POINT ( 'NONE',  ( 22.88900146558018989, 8.703904791123973084, -113.1500000000000483 ) ) ;
#54629=VERTEX_POINT ( 'NONE', #246850 ) ;
#54868=DIRECTION ( 'NONE',  ( 1.186688945009010077E-16, -1.000000000000000000, -0.000000000000000000 ) ) ;
#54958=FACE_OUTER_BOUND ( 'NONE', #93481, .T. ) ;
#54979=CARTESIAN_POINT ( 'NONE',  ( -16.89021194854739960, 9.950000000011138823, -121.2425681316043296 ) ) ;
#55066=CARTESIAN_POINT ( 'NONE',  ( -12.93407622233967835, 9.417789466963366607, -115.8573845439769059 ) ) ;
#55172=VERTEX_POINT ( 'NONE', #155199 ) ;
#55255=DIRECTION ( 'NONE',  ( 0.2834754621636358940, -0.2834754621636437211, 0.9161240771326893961 ) ) ;
#55464=VERTEX_POINT ( 'NONE', #194962 ) ;
#55484=DIRECTION ( 'NONE',  ( -1.000000000000000000, 0.000000000000000000, 0.000000000000000000 ) ) ;
#55555=CARTESIAN_POINT ( 'NONE',  ( -18.34374000495059676, 11.47316190337362940, -124.7500000000000426 ) ) ;
#55717=CARTESIAN_POINT ( 'NONE',  ( -15.55912972643741199, 8.490870273573719373, -113.0500000000000398 ) ) ;
#55835=DIRECTION ( 'NONE',  ( 1.000000000000000000, 0.000000000000000000, 0.000000000000000000 ) ) ;
#55944=CARTESIAN_POINT ( 'NONE',  ( -17.11825945287481332, 10.05000000001113847, -121.3500000000000369 ) ) ;
#56074=CARTESIAN_POINT ( 'NONE',  ( -16.92132318717937522, 9.966070024017081863, -113.1224066303521028 ) ) ;
#56173=CARTESIAN_POINT ( 'NONE',  ( -16.81453046979149235, 9.939102281452070642, -113.2117265236030335 ) ) ;
#56174=VECTOR ( 'NONE', #34011, 1000.000000000000000 ) ;
#56251=ORIENTED_EDGE ( 'NONE', *, *, #237777, .F. ) ;
#56252=FACE_OUTER_BOUND ( 'NONE', #221122, .T. ) ;
#56431=CARTESIAN_POINT ( 'NONE',  ( 20.04999999999999716, 8.750000000011173285, -113.1500000000000483 ) ) ;
#56503=CARTESIAN_POINT ( 'NONE',  ( -18.38204789744325396, 11.47950103717623982, -124.7500000000000284 ) ) ;
#56663=CARTESIAN_POINT ( 'NONE',  ( -15.75000000000000355, 9.350000000011140955, -117.2500000000000284 ) ) ;
#56670=DIRECTION ( 'NONE',  ( -1.000000000000000000, 1.652117596168391700E-15, 0.000000000000000000 ) ) ;
#56806=CARTESIAN_POINT ( 'NONE',  ( -16.86379686415369861, 9.975217759264314310, -113.0666101109097497 ) ) ;
#56964=EDGE_CURVE ( 'NONE', #15255, #89874, #220796, .T. ) ;
#57439=ADVANCED_FACE ( 'NONE', ( #106275 ), #79130, .T. ) ;
#57460=CARTESIAN_POINT ( 'NONE',  ( -16.87372386987899020, 9.880600233647912845, -113.6492698718664514 ) ) ;
#57582=EDGE_CURVE ( 'NONE', #80890, #55172, #171452, .T. ) ;
#57612=CARTESIAN_POINT ( 'NONE',  ( -16.94275863006528482, 9.989496048678669027, -121.3916973820766145 ) ) ;
#57970=DIRECTION ( 'NONE',  ( -1.652117596168391700E-15, -1.000000000000000000, 0.000000000000000000 ) ) ;
#58035=DIRECTION ( 'NONE',  ( 1.000000000000000000, 0.000000000000000000, -0.000000000000000000 ) ) ;
#58132=CARTESIAN_POINT ( 'NONE',  ( 21.72449340488910607, 10.28395627750227703, -109.7500000000000426 ) ) ;
#58352=DIRECTION ( 'NONE',  ( 1.000000000000000000, 0.000000000000000000, 0.000000000000000000 ) ) ;
#58425=CARTESIAN_POINT ( 'NONE',  ( -16.77683809663752257, 23.65833333334447985, -117.2500000000000284 ) ) ;
#58608=EDGE_CURVE ( 'NONE', #46173, #138239, #177317, .T. ) ;
#58656=ORIENTED_EDGE ( 'NONE', *, *, #187662, .F. ) ;
#58743=ORIENTED_EDGE ( 'NONE', *, *, #193878, .F. ) ;
#58836=CARTESIAN_POINT ( 'NONE',  ( -16.87333278164152972, 9.882609784590000501, -120.8668321938465482 ) ) ;
#59310=ORIENTED_EDGE ( 'NONE', *, *, #191929, .T. ) ;
#59521=ORIENTED_EDGE ( 'NONE', *, *, #63267, .T. ) ;
#59531=ORIENTED_EDGE ( 'NONE', *, *, #33898, .F. ) ;
#59753=CARTESIAN_POINT ( 'NONE',  ( -18.40000000000000213, 8.822561741677553471, -124.7500000000000284 ) ) ;
#59878=CARTESIAN_POINT ( 'NONE',  ( -18.37160782347004329, 11.47561641481354044, -109.7500000000000426 ) ) ;
#59882=ADVANCED_FACE ( 'NONE', ( #130124 ), #31073, .F. ) ;
#60063=( BOUNDED_SURFACE ( )  B_SPLINE_SURFACE ( 3, 2, ( 
 ( #79693, #158013, #138377 ),
 ( #103106, #182686, #217913 ),
 ( #58836, #4023, #83531 ),
 ( #237514, #38046, #163123 ),
 ( #22337, #39329, #238795 ),
 ( #118858, #1448, #101811 ),
 ( #198374, #99257, #178852 ),
 ( #240081, #160, #200944 ),
 ( #60133, #220520, #139660 ),
 ( #219212, #40632, #120166 ) ),
 .UNSPECIFIED., .F., .F., .F. ) 
 B_SPLINE_SURFACE_WITH_KNOTS ( ( 4, 2, 2, 2, 4 ),
 ( 3, 3 ),
 ( 0.002161241639767248670, 0.002579950749615824400, 0.002789305304540112482, 0.002893982582002256523, 0.002998659859464400564 ),
 ( 0.000000000000000000, 1.000000000000000000 ),
 .UNSPECIFIED. ) 
 GEOMETRIC_REPRESENTATION_ITEM ( )  RATIONAL_B_SPLINE_SURFACE ( (
 ( 1.000000000000000000, 0.7071067811865536790, 1.000000000000000000),
 ( 1.000000000000000000, 0.7632447400664197357, 1.000000000000000000),
 ( 1.000000000000000000, 0.8158073005110335618, 1.000000000000000000),
 ( 1.000000000000000000, 0.8906973462395710861, 1.000000000000000000),
 ( 1.000000000000000000, 0.9149408947800710123, 1.000000000000000000),
 ( 1.000000000000000000, 0.9493368785275515531, 1.000000000000000000),
 ( 1.000000000000000000, 0.9605194247156906284, 1.000000000000000000),
 ( 1.000000000000000000, 0.9803630264781052484, 1.000000000000000000),
 ( 1.000000000000000000, 0.9900844824271277655, 1.000000000000000000),
 ( 1.000000000000000000, 0.9894588281429246290, 1.000000000000000000) ) ) 
 REPRESENTATION_ITEM ( '' )  SURFACE ( )  );
#60124=EDGE_CURVE ( 'NONE', #137732, #67859, #191485, .T. ) ;
#60133=CARTESIAN_POINT ( 'NONE',  ( -16.79270642812318570, 9.946244216949072126, -121.3389332785620525 ) ) ;
#60134=EDGE_CURVE ( 'NONE', #78889, #107983, #175362, .T. ) ;
#60174=CARTESIAN_POINT ( 'NONE',  ( -17.04761207306817639, 10.02645087340892438, -121.3500000000000227 ) ) ;
#60612=DIRECTION ( 'NONE',  ( 0.000000000000000000, 0.000000000000000000, 1.000000000000000000 ) ) ;
#60645=VECTOR ( 'NONE', #50597, 1000.000000000000000 ) ;
#60718=CARTESIAN_POINT ( 'NONE',  ( -33.72168855820452649, 23.65833333334447985, -117.2500000000000284 ) ) ;
#60828=ORIENTED_EDGE ( 'NONE', *, *, #9915, .T. ) ;
#61066=LINE ( 'NONE', #140602, #158146 ) ;
#61153=ORIENTED_EDGE ( 'NONE', *, *, #168542, .F. ) ;
#61290=ORIENTED_EDGE ( 'NONE', *, *, #87589, .F. ) ;
#61368=CARTESIAN_POINT ( 'NONE',  ( -16.79184697841823493, 9.948761661669548673, -113.1541422706025486 ) ) ;
#61393=ORIENTED_EDGE ( 'NONE', *, *, #30461, .F. ) ;
#61636=VECTOR ( 'NONE', #186105, 1000.000000000000000 ) ;
#62090=CARTESIAN_POINT ( 'NONE',  ( -17.01764560440454588, 9.950000000011138823, -121.2500000007868408 ) ) ;
#62267=ORIENTED_EDGE ( 'NONE', *, *, #114152, .T. ) ;
#62483=CARTESIAN_POINT ( 'NONE',  ( 20.73486653747088582, 7.250000000011182166, -113.1500000000000483 ) ) ;
#62701=CARTESIAN_POINT ( 'NONE',  ( -18.40000000000000213, 11.75000000001113953, -124.7500000000000426 ) ) ;
#62807=CARTESIAN_POINT ( 'NONE',  ( -15.75000000000000355, 9.850000000011133849, -117.2500000000000284 ) ) ;
#62860=CARTESIAN_POINT ( 'NONE',  ( 16.87683809663750267, 9.950000000011138823, -113.1500000000000341 ) ) ;
#63131=EDGE_CURVE ( 'NONE', #78889, #33727, #76033, .T. ) ;
#63267=EDGE_CURVE ( 'NONE', #185216, #125547, #86641, .T. ) ;
#63281=CARTESIAN_POINT ( 'NONE',  ( 13.54556439290363379, 9.450592112144860835, -115.5561883188084664 ) ) ;
#63306=DIRECTION ( 'NONE',  ( -1.000000000000000000, 0.000000000000000000, 0.000000000000000000 ) ) ;
#63543=ORIENTED_EDGE ( 'NONE', *, *, #233639, .F. ) ;
#63557=LINE ( 'NONE', #144356, #233938 ) ;
#63577=LINE ( 'NONE', #66153, #63582 ) ;
#63582=VECTOR ( 'NONE', #179701, 1000.000000000000000 ) ;
#63754=FACE_OUTER_BOUND ( 'NONE', #234909, .T. ) ;
#63807=DIRECTION ( 'NONE',  ( 0.000000000000000000, 1.000000000000000000, 0.000000000000000000 ) ) ;
#63890=ORIENTED_EDGE ( 'NONE', *, *, #65234, .T. ) ;
#63895=CARTESIAN_POINT ( 'NONE',  ( -17.01764560440453522, 9.950000000011138823, -113.2499999992132302 ) ) ;
#63901=CARTESIAN_POINT ( 'NONE',  ( 20.73486653747088937, 7.750000000011182166, -113.1500000000000483 ) ) ;
#63942=CARTESIAN_POINT ( 'NONE',  ( -16.79814274880124358, 9.949272542688458287, -113.1524330370480271 ) ) ;
#64236=ORIENTED_EDGE ( 'NONE', *, *, #148852, .F. ) ;
#64393=CARTESIAN_POINT ( 'NONE',  ( -15.75000000000000355, 9.350000000011140955, -117.2500000000000284 ) ) ;
#64594=CARTESIAN_POINT ( 'NONE',  ( -16.87036670365548474, 9.989418819312801290, -121.4795601173020856 ) ) ;
#64643=CARTESIAN_POINT ( 'NONE',  ( 20.05000000000002913, 7.250000000011171508, -109.7500000000000426 ) ) ;
#64712=CARTESIAN_POINT ( 'NONE',  ( -12.30589683808040213, 9.356746017089404788, -117.7033597213642082 ) ) ;
#64905=LINE ( 'NONE', #188710, #52912 ) ;
#65039=DIRECTION ( 'NONE',  ( 1.000000000000000000, 0.000000000000000000, -0.000000000000000000 ) ) ;
#65164=EDGE_LOOP ( 'NONE', ( #250210, #92508, #146573, #2663 ) ) ;
#65234=EDGE_CURVE ( 'NONE', #146785, #104724, #73313, .T. ) ;
#65373=LINE ( 'NONE', #62807, #143077 ) ;
#65455=ORIENTED_EDGE ( 'NONE', *, *, #222160, .F. ) ;
#65517=ORIENTED_EDGE ( 'NONE', *, *, #79196, .F. ) ;
#65668=CARTESIAN_POINT ( 'NONE',  ( -17.11825945287482753, 9.950000000011138823, -113.2500000000000284 ) ) ;
#65812=EDGE_LOOP ( 'NONE', ( #25576, #49092, #25864, #15155, #162161, #106729 ) ) ;
#65851=CARTESIAN_POINT ( 'NONE',  ( 14.56326696814971022, 9.446648990640015953, -115.5891632959232140 ) ) ;
#65904=ORIENTED_EDGE ( 'NONE', *, *, #210925, .T. ) ;
#66060=CARTESIAN_POINT ( 'NONE',  ( -23.25000000000000355, 11.75000000001113953, -113.1500000000000341 ) ) ;
#66153=CARTESIAN_POINT ( 'NONE',  ( -16.77683809663752257, 9.950000000011138823, -121.3500000000000369 ) ) ;
#66183=AXIS2_PLACEMENT_3D ( 'NONE', #86202, #163215, #161940 ) ;
#66397=DIRECTION ( 'NONE',  ( -0.000000000000000000, -0.000000000000000000, -1.000000000000000000 ) ) ;
#66574=ORIENTED_EDGE ( 'NONE', *, *, #230518, .T. ) ;
#66646=VECTOR ( 'NONE', #204141, 1000.000000000000000 ) ;
#66716=CARTESIAN_POINT ( 'NONE',  ( -18.39999999999999858, 11.75000000001113953, -109.7500000000000426 ) ) ;
#66814=EDGE_LOOP ( 'NONE', ( #104509, #146003, #176972, #27164 ) ) ;
#66964=ADVANCED_FACE ( 'NONE', ( #177941 ), #257401, .F. ) ;
#67143=CARTESIAN_POINT ( 'NONE',  ( 15.75000000000000000, 9.350000000011137402, -117.0185689574026924 ) ) ;
#67278=CARTESIAN_POINT ( 'NONE',  ( -14.87770893841226894, 9.430637101707898040, -118.7682606180610065 ) ) ;
#67506=ORIENTED_EDGE ( 'NONE', *, *, #121542, .T. ) ;
#67525=LINE ( 'NONE', #241048, #223711 ) ;
#67722=DIRECTION ( 'NONE',  ( -1.020425574104004196E-15, 0.000000000000000000, -1.000000000000000000 ) ) ;
#67824=DIRECTION ( 'NONE',  ( -0.000000000000000000, -0.000000000000000000, -1.000000000000000000 ) ) ;
#67859=VERTEX_POINT ( 'NONE', #52593 ) ;
#68202=CARTESIAN_POINT ( 'NONE',  ( -18.40000000000000213, 11.47867410001106236, -124.7253067836594340 ) ) ;
#68401=CARTESIAN_POINT ( 'NONE',  ( -18.40000000000000213, 11.47316190337364183, -124.7500000000000426 ) ) ;
#68435=CARTESIAN_POINT ( 'NONE',  ( 15.52844286134407881, 9.375669526436931633, -116.3677900093859705 ) ) ;
#68508=CARTESIAN_POINT ( 'NONE',  ( -16.81744102076749314, 9.950000000011142376, -113.1500000000000341 ) ) ;
#68632=EDGE_LOOP ( 'NONE', ( #25179, #247982, #163233, #144088 ) ) ;
#68816=EDGE_CURVE ( 'NONE', #133581, #19091, #6114, .T. ) ;
#68962=CARTESIAN_POINT ( 'NONE',  ( -16.87383368123029825, 9.950000000011138823, -113.1500000000000341 ) ) ;
#69005=CARTESIAN_POINT ( 'NONE',  ( 18.54999999999999716, 8.750000000011173285, -113.1500000000000341 ) ) ;
#69048=ORIENTED_EDGE ( 'NONE', *, *, #138034, .T. ) ;
#69051=CARTESIAN_POINT ( 'NONE',  ( -16.95709691156327992, 9.950000000011140600, -113.1600575625087117 ) ) ;
#69387=ORIENTED_EDGE ( 'NONE', *, *, #224295, .T. ) ;
#69444=CYLINDRICAL_SURFACE ( 'NONE', #179615, 0.5000000000000004441 ) ;
#69544=CARTESIAN_POINT ( 'NONE',  ( -13.22483237240078857, 9.436674251854006101, -115.6768619309992658 ) ) ;
#69556=ORIENTED_EDGE ( 'NONE', *, *, #48663, .F. ) ;
#69596=ORIENTED_EDGE ( 'NONE', *, *, #172612, .F. ) ;
#69644=ADVANCED_FACE ( 'NONE', ( #204669 ), #179670, .T. ) ;
#69794=FACE_OUTER_BOUND ( 'NONE', #24755, .T. ) ;
#70055=CARTESIAN_POINT ( 'NONE',  ( -16.85722902420155478, 9.950000000011169021, -113.2655474737703116 ) ) ;
#70631=CARTESIAN_POINT ( 'NONE',  ( -23.25000000000000355, 5.650000000011139001, -121.3500000000000369 ) ) ;
#71014=ORIENTED_EDGE ( 'NONE', *, *, #256324, .F. ) ;
#71195=CARTESIAN_POINT ( 'NONE',  ( -16.93230518875208190, 10.00075036143099716, -113.0757783481015366 ) ) ;
#71336=CARTESIAN_POINT ( 'NONE',  ( -16.88705144915408951, 9.950000000011193890, -113.4309785947120872 ) ) ;
#71356=LINE ( 'NONE', #36074, #148803 ) ;
#71439=ORIENTED_EDGE ( 'NONE', *, *, #222613, .F. ) ;
#71501=VERTEX_POINT ( 'NONE', #84073 ) ;
#71546=VERTEX_POINT ( 'NONE', #82805 ) ;
#71563=DIRECTION ( 'NONE',  ( -0.000000000000000000, -0.000000000000000000, -1.000000000000000000 ) ) ;
#71600=LINE ( 'NONE', #131550, #168898 ) ;
#72028=VECTOR ( 'NONE', #191580, 1000.000000000000000 ) ;
#72107=CARTESIAN_POINT ( 'NONE',  ( -13.77178122865953824, 9.456028260519072859, -115.5111980350657745 ) ) ;
#72266=EDGE_LOOP ( 'NONE', ( #127334, #114967, #152587, #63543, #89216 ) ) ;
#72319=DIRECTION ( 'NONE',  ( 1.000000000000000000, -0.000000000000000000, -0.000000000000000000 ) ) ;
#72619=CARTESIAN_POINT ( 'NONE',  ( -16.85697194749131711, 9.908543714134740554, -113.4350042676143602 ) ) ;
#72629=CARTESIAN_POINT ( 'NONE',  ( 13.77030915526558630, 9.456007326080463571, -118.9886334941467965 ) ) ;
#72664=PRESENTATION_STYLE_ASSIGNMENT (( #154769 ) ) ;
#72785=LINE ( 'NONE', #152317, #60645 ) ;
#72943=LINE ( 'NONE', #151173, #251315 ) ;
#73068=VECTOR ( 'NONE', #111252, 999.9999999999998863 ) ;
#73131=CARTESIAN_POINT ( 'NONE',  ( -16.94445028196808778, 9.992063609708889516, -113.1073301784184792 ) ) ;
#73313=CIRCLE ( 'NONE', #235763, 0.1999999999999987899 ) ;
#73801=ORIENTED_EDGE ( 'NONE', *, *, #253395, .F. ) ;
#73811=CARTESIAN_POINT ( 'NONE',  ( 23.24999999999999645, 11.75000000001113953, -109.7500000000000426 ) ) ;
#73822=UNCERTAINTY_MEASURE_WITH_UNIT (LENGTH_MEASURE( 1.000000000000000082E-05 ), #175605, 'distance_accuracy_value', 'NONE');
#73881=ORIENTED_EDGE ( 'NONE', *, *, #29389, .T. ) ;
#73913=CARTESIAN_POINT ( 'NONE',  ( -16.84981964351502626, 9.917318234110025443, -113.3696016140195439 ) ) ;
#74332=ADVANCED_FACE ( 'NONE', ( #49481 ), #162936, .T. ) ;
#74422=CIRCLE ( 'NONE', #66183, 14.30833333333335311 ) ;
#74584=DIRECTION ( 'NONE',  ( -0.5932847527679299127, 0.8049926720990051576, 6.366092712777055223E-16 ) ) ;
#74592=DIRECTION ( 'NONE',  ( 0.000000000000000000, -0.000000000000000000, -1.000000000000000000 ) ) ;
#74946=CARTESIAN_POINT ( 'NONE',  ( 20.73486653747088582, 7.250000000011182166, -109.7500000000000426 ) ) ;
#74983=CARTESIAN_POINT ( 'NONE',  ( 13.99999999999999822, 9.850000000011137402, -117.2500000000000284 ) ) ;
#75060=CARTESIAN_POINT ( 'NONE',  ( -16.93583594267724024, 10.00862343506335783, -113.0593908393207840 ) ) ;
#75189=CARTESIAN_POINT ( 'NONE',  ( -16.77308656112214180, 9.950000000011135270, -113.1501931917023427 ) ) ;
#75261=FACE_OUTER_BOUND ( 'NONE', #128310, .T. ) ;
#75450=LINE ( 'NONE', #237062, #92764 ) ;
#75511=DIRECTION ( 'NONE',  ( 1.186688945009009831E-16, -1.000000000000000000, 0.000000000000000000 ) ) ;
#75516=VERTEX_POINT ( 'NONE', #239011 ) ;
#75693=CARTESIAN_POINT ( 'NONE',  ( -21.64999999999999858, 9.350000000011133849, -113.1500000000000341 ) ) ;
#75834=VERTEX_POINT ( 'NONE', #51041 ) ;
#75934=ORIENTED_EDGE ( 'NONE', *, *, #14131, .T. ) ;
#76033=B_SPLINE_CURVE_WITH_KNOTS ( 'NONE', 3,
 ( #39874, #37302, #157256, #56806, #119392, #136343, #198914, #20301, #99789, #686 ),
 .UNSPECIFIED., .F., .F.,
 ( 4, 3, 3, 4 ),
 ( 0.000000000000000000, 4.874959354401679605E-05, 9.785140065120178569E-05, 0.0001360444631935974781 ),
 .UNSPECIFIED. ) ;
#76118=EDGE_LOOP ( 'NONE', ( #179707, #249565 ) ) ;
#76247=CARTESIAN_POINT ( 'NONE',  ( 18.39999999999999503, 5.650000000011139001, -121.3500000000000369 ) ) ;
#76376=LINE ( 'NONE', #1976, #134495 ) ;
#76590=EDGE_CURVE ( 'NONE', #108024, #47116, #29659, .T. ) ;
#76720=ADVANCED_FACE ( 'NONE', ( #116854 ), #136377, .F. ) ;
#76797=ORIENTED_EDGE ( 'NONE', *, *, #45122, .F. ) ;
#77040=DIRECTION ( 'NONE',  ( -0.000000000000000000, -0.000000000000000000, -1.000000000000000000 ) ) ;
#77508=VERTEX_POINT ( 'NONE', #235858 ) ;
#77685=CARTESIAN_POINT ( 'NONE',  ( -16.87304349924914604, 9.961745077968330975, -121.3890666750452851 ) ) ;
#77844=CARTESIAN_POINT ( 'NONE',  ( -16.85312964099708211, 9.913604682078867469, -121.1028157064304622 ) ) ;
#77852=ORIENTED_EDGE ( 'NONE', *, *, #229143, .F. ) ;
#78207=CARTESIAN_POINT ( 'NONE',  ( -16.78805706634180339, 9.948252493082335945, -121.3441532080318979 ) ) ;
#78316=CARTESIAN_POINT ( 'NONE',  ( 23.24999999999999645, 8.822561741677553471, -109.7500000000000426 ) ) ;
#78432=ORIENTED_EDGE ( 'NONE', *, *, #154159, .F. ) ;
#78540=CARTESIAN_POINT ( 'NONE',  ( 12.25000000000000000, 9.350000000011140955, -117.2500000000000284 ) ) ;
#78857=VERTEX_POINT ( 'NONE', #189119 ) ;
#78889=VERTEX_POINT ( 'NONE', #239480 ) ;
#79130=( BOUNDED_SURFACE ( )  B_SPLINE_SURFACE ( 3, 2, ( 
 ( #64594, #166315, #128435 ),
 ( #25493, #204105, #247078 ),
 ( #146681, #124592, #144119 ),
 ( #104972, #167584, #48889 ) ),
 .UNSPECIFIED., .F., .F., .F. ) 
 B_SPLINE_SURFACE_WITH_KNOTS ( ( 4, 4 ),
 ( 3, 3 ),
 ( 0.0008258556059633754111, 0.0009616864997632845833 ),
 ( 0.000000000000000000, 1.000000000000000000 ),
 .UNSPECIFIED. ) 
 GEOMETRIC_REPRESENTATION_ITEM ( )  RATIONAL_B_SPLINE_SURFACE ( (
 ( 1.000000000000000000, 0.9152888060719386321, 1.000000000000000000),
 ( 1.000000000000000000, 0.9327727094138064112, 1.000000000000000000),
 ( 1.000000000000000000, 0.9369023509258621596, 1.000000000000000000),
 ( 1.000000000000000000, 0.9246339933864486937, 1.000000000000000000) ) ) 
 REPRESENTATION_ITEM ( '' )  SURFACE ( )  );
#79196=EDGE_CURVE ( 'NONE', #162352, #135449, #232986, .T. ) ;
#79209=CYLINDRICAL_SURFACE ( 'NONE', #81180, 1.749999999999998002 ) ;
#79390=SURFACE_SIDE_STYLE ('',( #257991 ) ) ;
#79605=ORIENTED_EDGE ( 'NONE', *, *, #210825, .F. ) ;
#79665=CYLINDRICAL_SURFACE ( 'NONE', #146777, 0.09999999999999939493 ) ;
#79693=CARTESIAN_POINT ( 'NONE',  ( -16.87683809663752399, 9.850000000011139178, -120.5976359818037196 ) ) ;
#79723=CARTESIAN_POINT ( 'NONE',  ( -16.98495255085916966, 10.00556436600592214, -121.3653827937795313 ) ) ;
#79886=ORIENTED_EDGE ( 'NONE', *, *, #221765, .T. ) ;
#79957=ORIENTED_EDGE ( 'NONE', *, *, #229143, .T. ) ;
#80067=DIRECTION ( 'NONE',  ( 1.000000000000000000, 0.000000000000000000, 1.073024830501117725E-15 ) ) ;
#80231=CARTESIAN_POINT ( 'NONE',  ( -16.86420534634261514, 9.970615445602874161, -121.4183365492374236 ) ) ;
#80254=CARTESIAN_POINT ( 'NONE',  ( 20.99999999999999645, 9.750000000011137757, -109.7500000000000426 ) ) ;
#80265=FACE_BOUND ( 'NONE', #76118, .T. ) ;
#80412=ORIENTED_EDGE ( 'NONE', *, *, #113172, .T. ) ;
#80730=CARTESIAN_POINT ( 'NONE',  ( -18.34804628011471195, 11.47316190337353525, -109.7500000000000426 ) ) ;
#80771=DIRECTION ( 'NONE',  ( -0.000000000000000000, 1.000000000000000000, -0.000000000000000000 ) ) ;
#80831=DIRECTION ( 'NONE',  ( 1.186688945009009831E-16, -1.000000000000000000, 0.000000000000000000 ) ) ;
#80890=VERTEX_POINT ( 'NONE', #223179 ) ;
#80967=EDGE_LOOP ( 'NONE', ( #67506, #183398 ) ) ;
#81002=LINE ( 'NONE', #19784, #247200 ) ;
#81180=AXIS2_PLACEMENT_3D ( 'NONE', #216160, #218719, #58352 ) ;
#81297=EDGE_LOOP ( 'NONE', ( #80412, #65904 ) ) ;
#81606=CARTESIAN_POINT ( 'NONE',  ( -17.11825945287481687, 9.950000000011140600, -121.3500000000000369 ) ) ;
#81709=CARTESIAN_POINT ( 'NONE',  ( -17.11825945287482753, 10.05000000001113847, -113.1500000000000341 ) ) ;
#81842=DIRECTION ( 'NONE',  ( -0.000000000000000000, 0.000000000000000000, -1.000000000000000000 ) ) ;
#82008=CARTESIAN_POINT ( 'NONE',  ( -16.93211319090181632, 9.999986781168624717, -121.4225054992731003 ) ) ;
#82304=ORIENTED_EDGE ( 'NONE', *, *, #25120, .T. ) ;
#82501=ADVANCED_FACE ( 'NONE', ( #43326 ), #45880, .F. ) ;
#82628=CARTESIAN_POINT ( 'NONE',  ( -14.77738660682463845, 9.436552840015579591, -115.6779554727603738 ) ) ;
#82705=EDGE_LOOP ( 'NONE', ( #97805, #150833, #220861, #220162 ) ) ;
#82799=CARTESIAN_POINT ( 'NONE',  ( -16.86578989773640913, 9.984809801269951990, -121.4646648866222733 ) ) ;
#82805=CARTESIAN_POINT ( 'NONE',  ( 23.24999999999999645, 11.75000000001113953, -113.1500000000000483 ) ) ;
#82985=ORIENTED_EDGE ( 'NONE', *, *, #206210, .F. ) ;
#83128=CARTESIAN_POINT ( 'NONE',  ( -23.25000000000000355, 10.05000000001113847, -113.2500000000000284 ) ) ;
#83248=ORIENTED_EDGE ( 'NONE', *, *, #195597, .T. ) ;
#83515=EDGE_CURVE ( 'NONE', #77508, #89874, #175211, .T. ) ;
#83531=CARTESIAN_POINT ( 'NONE',  ( -16.96982749440706328, 9.950000000011137047, -120.8752215911883070 ) ) ;
#83575=CARTESIAN_POINT ( 'NONE',  ( -17.11825945287481332, 9.950000000011138823, -121.2500000000000426 ) ) ;
#83643=LINE ( 'NONE', #163235, #159253 ) ;
#83836=LINE ( 'NONE', #225927, #256976 ) ;
#83882=EDGE_CURVE ( 'NONE', #34950, #133581, #100256, .T. ) ;
#83901=VERTEX_POINT ( 'NONE', #195733 ) ;
#83947=EDGE_LOOP ( 'NONE', ( #150947, #12697, #257806, #10098 ) ) ;
#83977=ORIENTED_EDGE ( 'NONE', *, *, #144120, .T. ) ;
#84073=CARTESIAN_POINT ( 'NONE',  ( -12.25000000000000178, 9.850000000011133849, -117.2500000000000284 ) ) ;
#84081=CARTESIAN_POINT ( 'NONE',  ( 15.74999999999999645, 9.350000000011139178, -117.2500000000000284 ) ) ;
#84107=CARTESIAN_POINT ( 'NONE',  ( 23.04999999999999716, 8.822561741677553471, -109.7500000000000426 ) ) ;
#84135=ORIENTED_EDGE ( 'NONE', *, *, #187472, .T. ) ;
#84267=DIRECTION ( 'NONE',  ( 0.000000000000000000, 0.000000000000000000, -1.000000000000000000 ) ) ;
#84631=ORIENTED_EDGE ( 'NONE', *, *, #199235, .T. ) ;
#84658=DIRECTION ( 'NONE',  ( -1.000000000000000000, 0.000000000000000000, 0.000000000000000000 ) ) ;
#84665=ORIENTED_EDGE ( 'NONE', *, *, #6035, .F. ) ;
#84909=AXIS2_PLACEMENT_3D ( 'NONE', #43915, #4759, #84267 ) ;
#85035=ORIENTED_EDGE ( 'NONE', *, *, #29598, .T. ) ;
#85178=CARTESIAN_POINT ( 'NONE',  ( -15.75000000000000355, 9.850000000011133849, -117.2500000000000284 ) ) ;
#85194=LINE ( 'NONE', #8280, #202156 ) ;
#85273=ORIENTED_EDGE ( 'NONE', *, *, #240855, .F. ) ;
#85409=FACE_OUTER_BOUND ( 'NONE', #41805, .T. ) ;
#85477=ADVANCED_FACE ( 'NONE', ( #29679 ), #203146, .T. ) ;
#85523=CARTESIAN_POINT ( 'NONE',  ( -13.11924609551134857, 9.431689550535258704, -118.7792900322360907 ) ) ;
#85670=ADVANCED_BREP_SHAPE_REPRESENTATION ( '', ( #107560, #2425 ), #252228 ) ;
#85832=VECTOR ( 'NONE', #128725, 1000.000000000000000 ) ;
#85989=CARTESIAN_POINT ( 'NONE',  ( -17.11825945287482753, 9.950000000011138823, -113.2500000000000426 ) ) ;
#86202=CARTESIAN_POINT ( 'NONE',  ( 18.54999999999999716, 23.65833333334447985, -117.2500000000000284 ) ) ;
#86364=ORIENTED_EDGE ( 'NONE', *, *, #105877, .F. ) ;
#86416=DIRECTION ( 'NONE',  ( -1.000000000000000000, 0.000000000000000000, 0.000000000000000000 ) ) ;
#86417=LINE ( 'NONE', #87715, #207017 ) ;
#86457=EDGE_LOOP ( 'NONE', ( #23241, #62267, #12154, #58743, #235992 ) ) ;
#86537=AXIS2_PLACEMENT_3D ( 'NONE', #17445, #55255, #134802 ) ;
#86553=ADVANCED_FACE ( 'NONE', ( #29727 ), #227892, .F. ) ;
#86628=AXIS2_PLACEMENT_3D ( 'NONE', #84107, #25491, #63306 ) ;
#86641=LINE ( 'NONE', #68401, #238974 ) ;
#86673=CARTESIAN_POINT ( 'NONE',  ( 12.93225390519044637, 9.417651958852159666, -115.8587873924405045 ) ) ;
#86776=CARTESIAN_POINT ( 'NONE',  ( -16.94107738177415712, 10.01423928514777728, -113.0500000000000398 ) ) ;
#86821=DIRECTION ( 'NONE',  ( 0.000000000000000000, -1.000000000000000000, 0.000000000000000000 ) ) ;
#86992=LINE ( 'NONE', #46588, #85832 ) ;
#87068=DIRECTION ( 'NONE',  ( -1.000000000000000000, 0.000000000000000000, 0.000000000000000000 ) ) ;
#87361=B_SPLINE_CURVE_WITH_KNOTS ( 'NONE', 3,
 ( #210297, #111188, #36820, #57612, #19809, #117605, #53775, #115038, #116336, #118907, #193303, #113743, #134575 ),
 .UNSPECIFIED., .F., .F.,
 ( 4, 3, 3, 3, 4 ),
 ( -3.224855718275878119E-06, 0.000000000000000000, 6.199515528665969596E-06, 4.034952380127732529E-05, 7.452715123699841550E-05 ),
 .UNSPECIFIED. ) ;
#87516=CARTESIAN_POINT ( 'NONE',  ( -16.87036670365549895, 9.989418819312803066, -113.0204398826979855 ) ) ;
#87589=EDGE_CURVE ( 'NONE', #229059, #112606, #118446, .T. ) ;
#87715=CARTESIAN_POINT ( 'NONE',  ( 20.73486653747090003, 7.250000000011182166, -121.3500000000000227 ) ) ;
#87780=CARTESIAN_POINT ( 'NONE',  ( -14.45443560709635911, 9.450592112144855506, -115.5561883188084096 ) ) ;
#87824=CARTESIAN_POINT ( 'NONE',  ( -16.87331047859649757, 9.950000000011138823, -121.3500000000000369 ) ) ;
#88104=CARTESIAN_POINT ( 'NONE',  ( -16.93344882324368683, 9.996588767299030565, -121.4130256948049578 ) ) ;
#88464=AXIS2_PLACEMENT_3D ( 'NONE', #133676, #56670, #57970 ) ;
#88473=CARTESIAN_POINT ( 'NONE',  ( -16.88560720703333473, 9.950564843760847822, -113.1481119208637551 ) ) ;
#88693=ORIENTED_EDGE ( 'NONE', *, *, #125000, .F. ) ;
#88755=CARTESIAN_POINT ( 'NONE',  ( -16.27683809663751191, 9.350000000011132073, -113.0500000000000398 ) ) ;
#88944=PLANE ( 'NONE',  #95241 ) ;
#89025=EDGE_CURVE ( 'NONE', #145735, #179299, #182480, .T. ) ;
#89044=ORIENTED_EDGE ( 'NONE', *, *, #228009, .T. ) ;
#89216=ORIENTED_EDGE ( 'NONE', *, *, #121954, .F. ) ;
#89352=VECTOR ( 'NONE', #149653, 1000.000000000000000 ) ;
#89370=DIRECTION ( 'NONE',  ( -1.000000000000000000, 0.000000000000000000, 0.000000000000000000 ) ) ;
#89400=CARTESIAN_POINT ( 'NONE',  ( -12.25000000000000178, 9.350000000011139178, -117.2500000000000284 ) ) ;
#89585=CARTESIAN_POINT ( 'NONE',  ( 15.73863059295127798, 9.351403174152808973, -117.4795304368385018 ) ) ;
#89593=CARTESIAN_POINT ( 'NONE',  ( -33.72168855820452649, 11.47316190337362940, -124.7500000000000426 ) ) ;
#89874=VERTEX_POINT ( 'NONE', #62860 ) ;
#90296=B_SPLINE_CURVE_WITH_KNOTS ( 'NONE', 3,
 ( #228014, #105457, #48084, #88473, #169365, #144603, #247573, #27283, #68962, #166789 ),
 .UNSPECIFIED., .F., .F.,
 ( 4, 3, 3, 4 ),
 ( 1.957469226477651626E-15, 8.145022132832446376E-06, 1.905645951092389470E-05, 2.061107371225767530E-05 ),
 .UNSPECIFIED. ) ;
#90602=CARTESIAN_POINT ( 'NONE',  ( 20.99999999999999645, 9.750000000011137757, -109.7500000000000426 ) ) ;
#90880=CARTESIAN_POINT ( 'NONE',  ( 15.66039659514495774, 9.360749169926259938, -117.8145701406072874 ) ) ;
#90932=FACE_OUTER_BOUND ( 'NONE', #48808, .T. ) ;
#91385=ORIENTED_EDGE ( 'NONE', *, *, #116881, .F. ) ;
#91439=EDGE_CURVE ( 'NONE', #80890, #221156, #10342, .T. ) ;
#91548=DIRECTION ( 'NONE',  ( -1.020425574104004196E-15, -1.210927747993693964E-31, 1.000000000000000000 ) ) ;
#91612=ORIENTED_EDGE ( 'NONE', *, *, #175632, .T. ) ;
#91630=EDGE_CURVE ( 'NONE', #100213, #71501, #164645, .T. ) ;
#91656=DIRECTION ( 'NONE',  ( 1.000000000000000000, 0.000000000000000000, 0.000000000000000000 ) ) ;
#92182=CYLINDRICAL_SURFACE ( 'NONE', #12543, 1.749999999999999778 ) ;
#92360=ORIENTED_EDGE ( 'NONE', *, *, #254760, .F. ) ;
#92458=DIRECTION ( 'NONE',  ( 1.000000000000000000, -0.000000000000000000, -0.000000000000000000 ) ) ;
#92508=ORIENTED_EDGE ( 'NONE', *, *, #132789, .F. ) ;
#92731=ORIENTED_EDGE ( 'NONE', *, *, #108872, .T. ) ;
#92764=VECTOR ( 'NONE', #135376, 1000.000000000000000 ) ;
#92765=AXIS2_PLACEMENT_3D ( 'NONE', #112262, #152686, #50958 ) ;
#92838=CARTESIAN_POINT ( 'NONE',  ( -16.94226253665224746, 9.950000000011137047, -121.0532654043842768 ) ) ;
#92867=FACE_OUTER_BOUND ( 'NONE', #72266, .T. ) ;
#92905=VECTOR ( 'NONE', #231234, 1000.000000000000000 ) ;
#93005=VERTEX_POINT ( 'NONE', #54411 ) ;
#93144=CARTESIAN_POINT ( 'NONE',  ( -17.78043020864320312, 10.85359211201683394, -110.8369508342798326 ) ) ;
#93174=ORIENTED_EDGE ( 'NONE', *, *, #126356, .F. ) ;
#93222=CARTESIAN_POINT ( 'NONE',  ( 17.23472005113827166, 10.30788195451192379, -122.5465768600687113 ) ) ;
#93429=CARTESIAN_POINT ( 'NONE',  ( -16.87683809663752754, 9.865889849343227880, -113.7674268070702936 ) ) ;
#93440=CARTESIAN_POINT ( 'NONE',  ( 12.84435279558019261, 9.410708747058235346, -118.5692084058441793 ) ) ;
#93481=EDGE_LOOP ( 'NONE', ( #79605, #182996, #48087 ) ) ;
#93641=DIRECTION ( 'NONE',  ( 1.186688945009010077E-16, -1.000000000000000000, -0.000000000000000000 ) ) ;
#93732=DIRECTION ( 'NONE',  ( 0.000000000000000000, 0.000000000000000000, 1.000000000000000000 ) ) ;
#94053=CARTESIAN_POINT ( 'NONE',  ( -18.40000000000000213, 11.47316190337364183, -124.6740539331920843 ) ) ;
#94104=DIRECTION ( 'NONE',  ( 0.000000000000000000, -1.000000000000000000, 0.000000000000000000 ) ) ;
#94124=CARTESIAN_POINT ( 'NONE',  ( -16.92989507731676468, 9.950000000011137047, -121.1174989306102390 ) ) ;
#94414=DIRECTION ( 'NONE',  ( 0.5932847527679310229, -0.8049926720990042694, -6.366092712777067056E-16 ) ) ;
#94426=EDGE_CURVE ( 'NONE', #40045, #38363, #193702, .T. ) ;
#94533=CARTESIAN_POINT ( 'NONE',  ( -16.91256925476569251, 9.985731158139328656, -121.4676424890052999 ) ) ;
#94629=CARTESIAN_POINT ( 'NONE',  ( -16.87331047859651179, 9.950000000011142376, -113.1500000000000341 ) ) ;
#94661=ORIENTED_EDGE ( 'NONE', *, *, #193878, .T. ) ;
#94717=CARTESIAN_POINT ( 'NONE',  ( -16.82542659449987354, 9.934499891438514751, -113.2446356000265268 ) ) ;
#94729=CARTESIAN_POINT ( 'NONE',  ( 12.42718393586866732, 9.370655051134638924, -118.0258232559809528 ) ) ;
#94788=CARTESIAN_POINT ( 'NONE',  ( -16.92209698673556417, 9.950000000011138823, -121.2893644329473659 ) ) ;
#94851=PLANE ( 'NONE',  #28255 ) ;
#95212=CARTESIAN_POINT ( 'NONE',  ( -16.77732147262506146, 9.945966932629787038, -121.3364912432759013 ) ) ;
#95241=AXIS2_PLACEMENT_3D ( 'NONE', #165959, #248027, #129372 ) ;
#95322=CARTESIAN_POINT ( 'NONE',  ( -16.85312841634287651, 9.913606177331356406, -113.3971731332925685 ) ) ;
#95397=PLANE ( 'NONE',  #5114 ) ;
#95494=ORIENTED_EDGE ( 'NONE', *, *, #198613, .T. ) ;
#95505=CARTESIAN_POINT ( 'NONE',  ( -16.87331047859651179, 9.950000000011142376, -113.1500000000000341 ) ) ;
#95661=ORIENTED_EDGE ( 'NONE', *, *, #233639, .T. ) ;
#95937=ADVANCED_FACE ( 'NONE', ( #54508 ), #197863, .F. ) ;
#96037=SURFACE_STYLE_FILL_AREA ( #217258 ) ;
#96058=CARTESIAN_POINT ( 'NONE',  ( -16.92570016628984320, 9.958788957751014692, -113.1206506700390406 ) ) ;
#96105=CARTESIAN_POINT ( 'NONE',  ( -15.75000000000000355, 9.350000000011140955, -117.2500000000000284 ) ) ;
#96647=DIRECTION ( 'NONE',  ( -0.000000000000000000, -0.000000000000000000, -1.000000000000000000 ) ) ;
#96951=DIRECTION ( 'NONE',  ( 1.000000000000000000, 0.000000000000000000, 0.000000000000000000 ) ) ;
#97100=EDGE_CURVE ( 'NONE', #83901, #179299, #33874, .T. ) ;
#97263=APPLICATION_CONTEXT ( 'automotive_design' ) ;
#97293=SURFACE_SIDE_STYLE ('',( #96037 ) ) ;
#97600=ADVANCED_FACE ( 'NONE', ( #56252 ), #95397, .T. ) ;
#97615=ORIENTED_EDGE ( 'NONE', *, *, #105654, .F. ) ;
#97644=EDGE_CURVE ( 'NONE', #21871, #256969, #242656, .T. ) ;
#97662=ADVANCED_FACE ( 'NONE', ( #223040 ), #79665, .F. ) ;
#97715=CARTESIAN_POINT ( 'NONE',  ( -18.40000000000000213, 11.48667500176882328, -109.7500000000000426 ) ) ;
#97805=ORIENTED_EDGE ( 'NONE', *, *, #57582, .T. ) ;
#98162=CARTESIAN_POINT ( 'NONE',  ( 20.99999999999999645, 9.750000000011137757, -113.1500000000000483 ) ) ;
#98522=CARTESIAN_POINT ( 'NONE',  ( -17.22361732159831860, 10.34515565861359399, -122.6292154741329199 ) ) ;
#98573=CIRCLE ( 'NONE', #11149, 0.09999999999999939493 ) ;
#98659=CARTESIAN_POINT ( 'NONE',  ( -16.83794479845801817, 9.926357419362648926, -121.1964447042223441 ) ) ;
#98783=CIRCLE ( 'NONE', #202869, 0.9000000000000014655 ) ;
#98939=FILL_AREA_STYLE_COLOUR ( '', #56 ) ;
#99257=CARTESIAN_POINT ( 'NONE',  ( -16.84793658983413422, 9.950000000011076651, -121.2663533221895875 ) ) ;
#99681=VECTOR ( 'NONE', #10789, 999.9999999999998863 ) ;
#99759=LINE ( 'NONE', #41124, #257869 ) ;
#99789=CARTESIAN_POINT ( 'NONE',  ( -16.88495309932521593, 9.954627058484010860, -113.1345486738119490 ) ) ;
#100213=VERTEX_POINT ( 'NONE', #85178 ) ;
#100224=PRESENTATION_STYLE_ASSIGNMENT (( #158978 ) ) ;
#100256=B_SPLINE_CURVE_WITH_KNOTS ( 'NONE', 3,
 ( #236112, #138275, #178752, #199587, #118753, #56173, #213990, #39226, #159176, #95322, #174917, #57460, #254367, #238682 ),
 .UNSPECIFIED., .F., .F.,
 ( 4, 2, 2, 2, 2, 2, 4 ),
 ( 0.000000000000000000, 2.389617747640384587E-05, 4.779235495280769174E-05, 9.558470990564789599E-05, 0.0001911694198113680541, 0.0003823388396228101049, 0.0007646776792456942608 ),
 .UNSPECIFIED. ) ;
#100989=AXIS2_PLACEMENT_3D ( 'NONE', #2073, #161174, #240708 ) ;
#101219=CARTESIAN_POINT ( 'NONE',  ( -16.85939681242906119, 9.905225185936462395, -121.0399219551915166 ) ) ;
#101250=AXIS2_PLACEMENT_3D ( 'NONE', #83128, #38926, #162725 ) ;
#101299=ORIENTED_EDGE ( 'NONE', *, *, #1505, .T. ) ;
#101440=AXIS2_PLACEMENT_3D ( 'NONE', #11427, #107943, #205751 ) ;
#101548=CARTESIAN_POINT ( 'NONE',  ( -23.25000000000000355, 10.05000000001113847, -121.2500000000000426 ) ) ;
#101707=ADVANCED_FACE ( 'NONE', ( #220347 ), #222886, .F. ) ;
#101765=EDGE_CURVE ( 'NONE', #228258, #162005, #3855, .T. ) ;
#101811=CARTESIAN_POINT ( 'NONE',  ( -16.88783316861814399, 9.950000000011137047, -121.2477359580202716 ) ) ;
#102019=CIRCLE ( 'NONE', #177084, 1.500000000000001332 ) ;
#102361=EDGE_CURVE ( 'NONE', #71546, #110479, #32111, .T. ) ;
#102609=( BOUNDED_SURFACE ( )  B_SPLINE_SURFACE ( 3, 2, ( 
 ( #38428, #94533, #119258 ),
 ( #137502, #136203, #198771 ),
 ( #20158, #217039, #560 ),
 ( #174132, #253603, #134923 ) ),
 .UNSPECIFIED., .F., .F., .T. ) 
 B_SPLINE_SURFACE_WITH_KNOTS ( ( 4, 4 ),
 ( 3, 3 ),
 ( 0.3000847527772381729, 0.5552748953338751958 ),
 ( 0.000000000000000000, 1.000000000000000000 ),
 .UNSPECIFIED. ) 
 GEOMETRIC_REPRESENTATION_ITEM ( )  RATIONAL_B_SPLINE_SURFACE ( (
 ( 1.000000000000000000, 0.9152888060719386321, 1.000000000000000000),
 ( 1.000000000000000000, 0.9104333467450184125, 1.000000000000000000),
 ( 1.000000000000000000, 0.9035312726220658952, 1.000000000000000000),
 ( 1.000000000000000000, 0.8946697475932153809, 1.000000000000000000) ) ) 
 REPRESENTATION_ITEM ( '' )  SURFACE ( )  );
#102778=FACE_OUTER_BOUND ( 'NONE', #165149, .T. ) ;
#102858=DIRECTION ( 'NONE',  ( -0.000000000000000000, 0.000000000000000000, -1.000000000000000000 ) ) ;
#103106=CARTESIAN_POINT ( 'NONE',  ( -16.87683809663752399, 9.865889849343686180, -120.7325731929305732 ) ) ;
#103203=FACE_OUTER_BOUND ( 'NONE', #68632, .T. ) ;
#103263=CARTESIAN_POINT ( 'NONE',  ( -20.65000000000000568, 7.250000000011138646, -109.7500000000000426 ) ) ;
#103602=DIRECTION ( 'NONE',  ( -0.000000000000000000, -0.000000000000000000, -1.000000000000000000 ) ) ;
#103649=DIRECTION ( 'NONE',  ( -1.073024830501117725E-15, -0.000000000000000000, -1.000000000000000000 ) ) ;
#104191=ADVANCED_FACE ( 'NONE', ( #132577 ), #133196, .F. ) ;
#104501=CARTESIAN_POINT ( 'NONE',  ( -17.22361732159832215, 10.34515565861359221, -111.8707845258671654 ) ) ;
#104509=ORIENTED_EDGE ( 'NONE', *, *, #116054, .F. ) ;
#104512=VERTEX_POINT ( 'NONE', #113977 ) ;
#104686=DIRECTION ( 'NONE',  ( 1.000000000000000000, 1.646408749285562691E-14, 1.073024830501117725E-15 ) ) ;
#104724=VERTEX_POINT ( 'NONE', #184223 ) ;
#104945=CARTESIAN_POINT ( 'NONE',  ( 13.88302573338718560, 9.457410944778565920, -115.5000839737900833 ) ) ;
#104971=CARTESIAN_POINT ( 'NONE',  ( 20.05000000000002913, 7.250000000011171508, -121.3500000000000227 ) ) ;
#104972=CARTESIAN_POINT ( 'NONE',  ( -16.89318236219975589, 9.951535257886286345, -121.3551296321058857 ) ) ;
#104985=ORIENTED_EDGE ( 'NONE', *, *, #83882, .F. ) ;
#105155=VECTOR ( 'NONE', #13185, 1000.000000000000000 ) ;
#105457=CARTESIAN_POINT ( 'NONE',  ( -16.89060415895971090, 9.951220762813354881, -113.1459202242704976 ) ) ;
#105539=VERTEX_POINT ( 'NONE', #188416 ) ;
#105569=ORIENTED_EDGE ( 'NONE', *, *, #13775, .T. ) ;
#105654=EDGE_CURVE ( 'NONE', #230044, #19091, #98573, .T. ) ;
#105877=EDGE_CURVE ( 'NONE', #28001, #110479, #83836, .T. ) ;
#105894=AXIS2_PLACEMENT_3D ( 'NONE', #174429, #12761, #175676 ) ;
#105934=AXIS2_PLACEMENT_3D ( 'NONE', #179319, #60612, #58035 ) ;
#105968=DIRECTION ( 'NONE',  ( 1.000000000000000000, -0.000000000000000000, -0.000000000000000000 ) ) ;
#106244=CARTESIAN_POINT ( 'NONE',  ( 13.76927104934456914, 9.455987233623899257, -115.5115311668978677 ) ) ;
#106275=FACE_OUTER_BOUND ( 'NONE', #163292, .T. ) ;
#106317=CARTESIAN_POINT ( 'NONE',  ( -16.97683809663753252, 9.950000000011138823, -113.7715247686699769 ) ) ;
#106458=COLOUR_RGB ( '', 0.40784314, 0.44705882, 0.49803922) ;
#106502=B_SPLINE_CURVE_WITH_KNOTS ( 'NONE', 3,
 ( #15710, #95212, #176064, #196872, #238571, #78207, #14422, #254266, #255514, #258085 ),
 .UNSPECIFIED., .F., .F.,
 ( 4, 3, 3, 4 ),
 ( -2.000561356210515597E-06, 0.000000000000000000, 1.787822682428821068E-05, 4.206475347089863842E-05 ),
 .UNSPECIFIED. ) ;
#106514=CARTESIAN_POINT ( 'NONE',  ( -23.25000000000000355, 11.75000000001113953, -124.7500000000000284 ) ) ;
#106591=DIRECTION ( 'NONE',  ( 1.186688945009009831E-16, -1.000000000000000000, 0.000000000000000000 ) ) ;
#106729=ORIENTED_EDGE ( 'NONE', *, *, #156590, .T. ) ;
#106745=VERTEX_POINT ( 'NONE', #34890 ) ;
#106861=LINE ( 'NONE', #186430, #72028 ) ;
#107063=ORIENTED_EDGE ( 'NONE', *, *, #29141, .F. ) ;
#107168=LINE ( 'NONE', #186734, #215137 ) ;
#107289=ORIENTED_EDGE ( 'NONE', *, *, #29871, .F. ) ;
#107560=MANIFOLD_SOLID_BREP ( 'Stock-MAS-200-1', #111715 ) ;
#107616=CARTESIAN_POINT ( 'NONE',  ( -16.89268316805465986, 9.951721813253337601, -121.3557524785455826 ) ) ;
#107685=CARTESIAN_POINT ( 'NONE',  ( -13.77083647240106323, 9.457410930301319851, -118.9999159087463454 ) ) ;
#107936=DIRECTION ( 'NONE',  ( -0.7071067811865487940, 0.7071067811865463515, 0.000000000000000000 ) ) ;
#107943=DIRECTION ( 'NONE',  ( 0.000000000000000000, 0.000000000000000000, 1.000000000000000000 ) ) ;
#107983=VERTEX_POINT ( 'NONE', #86776 ) ;
#108024=VERTEX_POINT ( 'NONE', #133622 ) ;
#108025=CARTESIAN_POINT ( 'NONE',  ( -18.40000000000000213, 11.47316190337364183, -121.3914213562373448 ) ) ;
#108133=EDGE_LOOP ( 'NONE', ( #227560, #236209, #6832, #39927 ) ) ;
#108381=AXIS2_PLACEMENT_3D ( 'NONE', #101548, #242370, #2469 ) ;
#108391=ADVANCED_FACE ( 'NONE', ( #151636 ), #188169, .F. ) ;
#108872=EDGE_CURVE ( 'NONE', #19091, #121961, #119508, .T. ) ;
#108973=CARTESIAN_POINT ( 'NONE',  ( -16.93353400591625757, 10.00461239618409515, -121.4326844702054444 ) ) ;
#109435=CARTESIAN_POINT ( 'NONE',  ( -18.41431012584569160, 11.48747202921932242, -109.7267639868983480 ) ) ;
#109485=LINE ( 'NONE', #230749, #198230 ) ;
#109857=CYLINDRICAL_SURFACE ( 'NONE', #29321, 0.1000000000000013656 ) ;
#109876=CARTESIAN_POINT ( 'NONE',  ( -18.40000000000000213, 11.47316190337310893, -124.7001707515342872 ) ) ;
#110111=EDGE_CURVE ( 'NONE', #121961, #78857, #106502, .T. ) ;
#110115=ORIENTED_EDGE ( 'NONE', *, *, #249812, .T. ) ;
#110295=CARTESIAN_POINT ( 'NONE',  ( -18.39999999999999858, 11.47316190337362762, -109.7998292484660539 ) ) ;
#110479=VERTEX_POINT ( 'NONE', #22776 ) ;
#110609=ORIENTED_EDGE ( 'NONE', *, *, #216957, .T. ) ;
#110647=ADVANCED_FACE ( 'NONE', ( #216653 ), #60063, .F. ) ;
#110794=VECTOR ( 'NONE', #199795, 1000.000000000000000 ) ;
#111188=CARTESIAN_POINT ( 'NONE',  ( -16.94389599337535657, 9.991197989767881538, -121.3923551982016420 ) ) ;
#111191=CARTESIAN_POINT ( 'NONE',  ( 20.73486653747088937, 7.750000000011182166, -121.3500000000000227 ) ) ;
#111252=DIRECTION ( 'NONE',  ( 0.5932847527679299127, -0.8049926720990051576, 6.366092712777055223E-16 ) ) ;
#111273=AXIS2_PLACEMENT_3D ( 'NONE', #151659, #12146, #91656 ) ;
#111422=ORIENTED_EDGE ( 'NONE', *, *, #168542, .T. ) ;
#111591=CARTESIAN_POINT ( 'NONE',  ( -16.93302609847409457, 9.996682520814371031, -113.0863884953625842 ) ) ;
#111715=CLOSED_SHELL ( 'NONE', ( #233123, #95937, #202520, #135911, #101707, #86553, #148733, #167086, #59882, #191811, #149768, #138124, #205431, #46625, #174183, #82501, #250160, #38493, #163363, #230972, #131071, #194549, #38180, #76720, #129065, #129649, #66964, #43278, #120560, #235760, #108391, #238642, #257314, #85477, #224906, #197222, #136556, #185392, #97600, #52904, #110647, #97662, #104191, #245431, #118848, #74332, #191844, #256533, #69644, #238099, #57439, #159997, #146677 ) ) ;
#112030=DIRECTION ( 'NONE',  ( 0.000000000000000000, -1.000000000000000000, 0.000000000000000000 ) ) ;
#112045=EDGE_CURVE ( 'NONE', #38363, #49384, #87361, .T. ) ;
#112262=CARTESIAN_POINT ( 'NONE',  ( -21.65000000000000213, 7.250000000011138646, -109.7500000000000426 ) ) ;
#112305=LINE ( 'NONE', #70631, #138175 ) ;
#112388=LINE ( 'NONE', #246738, #27453 ) ;
#112572=LINE ( 'NONE', #154306, #33404 ) ;
#112606=VERTEX_POINT ( 'NONE', #160306 ) ;
#112876=ORIENTED_EDGE ( 'NONE', *, *, #137237, .T. ) ;
#112918=DIRECTION ( 'NONE',  ( 0.000000000000000000, 0.000000000000000000, -1.000000000000000000 ) ) ;
#113011=CARTESIAN_POINT ( 'NONE',  ( -16.77180007708460607, 9.950000000011137047, -113.1356141189548623 ) ) ;
#113169=EDGE_CURVE ( 'NONE', #141252, #15255, #125958, .T. ) ;
#113172=EDGE_CURVE ( 'NONE', #44121, #181223, #195919, .T. ) ;
#113528=ORIENTED_EDGE ( 'NONE', *, *, #63131, .F. ) ;
#113551=ORIENTED_EDGE ( 'NONE', *, *, #105654, .T. ) ;
#113743=CARTESIAN_POINT ( 'NONE',  ( -16.90128866880176162, 9.953795777214113016, -121.3626761833886718 ) ) ;
#113831=CARTESIAN_POINT ( 'NONE',  ( -17.01473183483379970, 9.950000000011140600, -121.2500000000000284 ) ) ;
#113977=CARTESIAN_POINT ( 'NONE',  ( 18.54999999999999716, 8.750000000011182166, -121.3500000000000369 ) ) ;
#113998=EDGE_CURVE ( 'NONE', #168103, #245454, #214837, .T. ) ;
#114008=DIRECTION ( 'NONE',  ( -1.000000000000000000, 0.000000000000000000, 0.000000000000000000 ) ) ;
#114144=CARTESIAN_POINT ( 'NONE',  ( -16.94180778212362881, 9.992443055743304825, -113.1041835705332801 ) ) ;
#114152=EDGE_CURVE ( 'NONE', #163086, #14870, #211624, .T. ) ;
#114160=VECTOR ( 'NONE', #77040, 1000.000000000000000 ) ;
#114297=CARTESIAN_POINT ( 'NONE',  ( 15.07585980824113925, 9.417632963117448242, -118.6489484657323175 ) ) ;
#114459=DIRECTION ( 'NONE',  ( -0.000000000000000000, 1.000000000000000000, -0.000000000000000000 ) ) ;
#114471=CARTESIAN_POINT ( 'NONE',  ( -21.65000000000000213, 7.250000000011139534, -121.3500000000000369 ) ) ;
#114716=EDGE_CURVE ( 'NONE', #209604, #233466, #38702, .T. ) ;
#114719=VECTOR ( 'NONE', #244168, 1000.000000000000000 ) ;
#114921=EDGE_CURVE ( 'NONE', #26064, #168680, #106861, .T. ) ;
#114967=ORIENTED_EDGE ( 'NONE', *, *, #186197, .T. ) ;
#115038=CARTESIAN_POINT ( 'NONE',  ( -16.93301857435212554, 9.976309354746611291, -121.3857755711614601 ) ) ;
#115160=ORIENTED_EDGE ( 'NONE', *, *, #124916, .T. ) ;
#115300=CARTESIAN_POINT ( 'NONE',  ( -16.97683809663752186, 9.850000000011137402, -120.5976359818037196 ) ) ;
#115398=CARTESIAN_POINT ( 'NONE',  ( -23.25000000000000355, 11.75000000001113953, -109.7500000000000426 ) ) ;
#115427=CARTESIAN_POINT ( 'NONE',  ( -16.93339986808596720, 10.00510392857707664, -113.0659936718128904 ) ) ;
#115568=CARTESIAN_POINT ( 'NONE',  ( -16.77431908686106254, 9.945805754529134290, -113.1641607823497964 ) ) ;
#115612=EDGE_LOOP ( 'NONE', ( #175447, #246915, #41127, #176821, #150693 ) ) ;
#115711=DIRECTION ( 'NONE',  ( 0.000000000000000000, 1.000000000000000000, -0.000000000000000000 ) ) ;
#116054=EDGE_CURVE ( 'NONE', #145735, #75834, #246958, .T. ) ;
#116257=CARTESIAN_POINT ( 'NONE',  ( 16.27683809663749770, 9.350000000011137402, -109.7500000000000426 ) ) ;
#116336=CARTESIAN_POINT ( 'NONE',  ( -16.92563707711778065, 9.968990694407935393, -121.3807582995240040 ) ) ;
#116647=FACE_OUTER_BOUND ( 'NONE', #66814, .T. ) ;
#116809=PLANE ( 'NONE',  #234465 ) ;
#116854=FACE_OUTER_BOUND ( 'NONE', #142746, .T. ) ;
#116881=EDGE_CURVE ( 'NONE', #189017, #52458, #130992, .T. ) ;
#116900=( NAMED_UNIT ( * ) PLANE_ANGLE_UNIT ( ) SI_UNIT ( $, .RADIAN. ) );
#117133=DIRECTION ( 'NONE',  ( 1.186688945009009831E-16, -1.000000000000000000, 0.000000000000000000 ) ) ;
#117363=CARTESIAN_POINT ( 'NONE',  ( -16.94275863009466576, 9.989496048673542461, -113.1083026179589126 ) ) ;
#117523=ORIENTED_EDGE ( 'NONE', *, *, #202822, .T. ) ;
#117592=CARTESIAN_POINT ( 'NONE',  ( -16.94445028196807002, 9.992063609708893068, -121.3926698215815918 ) ) ;
#117605=CARTESIAN_POINT ( 'NONE',  ( -16.94052228080551359, 9.986279733109993728, -121.3903755026694569 ) ) ;
#117951=ORIENTED_EDGE ( 'NONE', *, *, #222809, .T. ) ;
#117972=PLANE ( 'NONE',  #200201 ) ;
#118190=AXIS2_PLACEMENT_3D ( 'NONE', #182542, #80831, #143389 ) ;
#118446=CIRCLE ( 'NONE', #180981, 0.5000000000000004441 ) ;
#118662=DIRECTION ( 'NONE',  ( 1.186688945009010077E-16, -1.000000000000000000, -0.000000000000000000 ) ) ;
#118691=( BOUNDED_CURVE ( )  B_SPLINE_CURVE ( 3, ( #117592, #79723, #60174, #197117 ),
 .UNSPECIFIED., .F., .F. ) 
 B_SPLINE_CURVE_WITH_KNOTS ( ( 4, 4 ),
 ( 3.752122642744613046, 4.712388980384671910 ),
 .UNSPECIFIED. ) 
 CURVE ( )  GEOMETRIC_REPRESENTATION_ITEM ( )  RATIONAL_B_SPLINE_CURVE ( ( 1.000000000000000000, 0.9246222802177266331, 0.9246222802177266331, 1.000000000000000000 ) ) 
 REPRESENTATION_ITEM ( '' )  );
#118753=CARTESIAN_POINT ( 'NONE',  ( -16.80468759584937999, 9.942153675145299019, -113.1900188662016831 ) ) ;
#118848=ADVANCED_FACE ( 'NONE', ( #92867 ), #109857, .F. ) ;
#118858=CARTESIAN_POINT ( 'NONE',  ( -16.83233564386403458, 9.930221796595763095, -121.2245206634756585 ) ) ;
#118907=CARTESIAN_POINT ( 'NONE',  ( -16.91776028072577631, 9.963400393640901243, -121.3750240147021486 ) ) ;
#119004=ORIENTED_EDGE ( 'NONE', *, *, #132789, .T. ) ;
#119258=CARTESIAN_POINT ( 'NONE',  ( -16.87036670365548474, 9.989418819312799513, -121.4795601173020856 ) ) ;
#119366=AXIS2_PLACEMENT_3D ( 'NONE', #168655, #246840, #8255 ) ;
#119392=CARTESIAN_POINT ( 'NONE',  ( -16.86422026484316916, 9.970447360871810716, -113.0822132256730299 ) ) ;
#119508=B_SPLINE_CURVE_WITH_KNOTS ( 'NONE', 3,
 ( #150984, #255151, #212253, #101219, #77844, #98659, #256422, #180817, #141671, #2153, #37465, #235636, #42575, #240787 ),
 .UNSPECIFIED., .F., .F.,
 ( 4, 2, 2, 2, 2, 2, 4 ),
 ( 1.398578778534940505E-17, 0.0003823333598418207288, 0.0005735000397627034461, 0.0006690833797231245843, 0.0007168750497033337440, 0.0007407708846934382696, 0.0007646667196835427952 ),
 .UNSPECIFIED. ) ;
#119562=CARTESIAN_POINT ( 'NONE',  ( -16.97683809663752186, 9.950000000011138823, -109.7500000000000426 ) ) ;
#119843=CARTESIAN_POINT ( 'NONE',  ( -16.97683809663752186, 9.950000000011138823, -120.5976359818037196 ) ) ;
#119992=DIRECTION ( 'NONE',  ( -0.000000000000000000, -0.000000000000000000, -1.000000000000000000 ) ) ;
#120166=CARTESIAN_POINT ( 'NONE',  ( -16.77180007708460607, 9.950000000011137047, -121.3643858810452087 ) ) ;
#120258=CARTESIAN_POINT ( 'NONE',  ( 20.27550659511089037, 9.216043722520002035, -113.1500000000000483 ) ) ;
#120274=LINE ( 'NONE', #220623, #110794 ) ;
#120460=CARTESIAN_POINT ( 'NONE',  ( 20.73486653747088582, 7.250000000011182166, -121.3500000000000227 ) ) ;
#120560=ADVANCED_FACE ( 'NONE', ( #63754 ), #224106, .F. ) ;
#120688=DIRECTION ( 'NONE',  ( -1.000000000000000000, 0.000000000000000000, 0.000000000000000000 ) ) ;
#120707=EDGE_LOOP ( 'NONE', ( #117951, #60828, #51854, #48550 ) ) ;
#121173=CARTESIAN_POINT ( 'NONE',  ( 18.39999999999999503, 11.47316190337363828, -113.1500000000000341 ) ) ;
#121387=CARTESIAN_POINT ( 'NONE',  ( -16.77683809663752257, 9.945835743215301505, -113.1639490191042512 ) ) ;
#121516=EDGE_CURVE ( 'NONE', #75834, #83901, #249504, .T. ) ;
#121539=DIRECTION ( 'NONE',  ( -1.020425574104004196E-15, 0.000000000000000000, 1.000000000000000000 ) ) ;
#121542=EDGE_CURVE ( 'NONE', #71501, #100213, #167969, .T. ) ;
#121791=ORIENTED_EDGE ( 'NONE', *, *, #33898, .T. ) ;
#121954=EDGE_CURVE ( 'NONE', #40045, #125547, #248265, .T. ) ;
#121961=VERTEX_POINT ( 'NONE', #188282 ) ;
#121971=CARTESIAN_POINT ( 'NONE',  ( -16.88460203013675454, 9.954759003246872240, -121.3658918095382546 ) ) ;
#122620=PRODUCT ( 'Snap Open Cable Crossbars 4', 'Snap Open Cable Crossbars 4', '', ( #7671 ) ) ;
#122635=VERTEX_POINT ( 'NONE', #126409 ) ;
#122651=CARTESIAN_POINT ( 'NONE',  ( -16.78055652883087134, 9.946776916136505164, -113.1607918375924697 ) ) ;
#123265=CARTESIAN_POINT ( 'NONE',  ( 15.15590539855246099, 9.410682294279107296, -115.9311434419482936 ) ) ;
#123411=VECTOR ( 'NONE', #80771, 1000.000000000000000 ) ;
#124011=CARTESIAN_POINT ( 'NONE',  ( -18.40000000000000213, 11.48667500176882328, -109.7500000000000426 ) ) ;
#124373=CARTESIAN_POINT ( 'NONE',  ( -14.87779219673429409, 9.430633469083950615, -115.7317657948241560 ) ) ;
#124491=CARTESIAN_POINT ( 'NONE',  ( -20.65000000000000568, 5.650000000011139001, -109.7500000000000426 ) ) ;
#124592=CARTESIAN_POINT ( 'NONE',  ( -16.90202395485776776, 9.965944544561994078, -121.4030137212604501 ) ) ;
#124627=LINE ( 'NONE', #64643, #66646 ) ;
#124798=EDGE_LOOP ( 'NONE', ( #220511, #170236, #252, #247754 ) ) ;
#124847=ORIENTED_EDGE ( 'NONE', *, *, #83515, .F. ) ;
#124916=EDGE_CURVE ( 'NONE', #45147, #21871, #109485, .T. ) ;
#125000=EDGE_CURVE ( 'NONE', #200735, #146785, #48240, .T. ) ;
#125364=CARTESIAN_POINT ( 'NONE',  ( 18.39999999999999503, 5.650000000011139001, -113.1500000000000341 ) ) ;
#125547=VERTEX_POINT ( 'NONE', #173535 ) ;
#125615=EDGE_CURVE ( 'NONE', #105539, #52458, #219012, .T. ) ;
#125822=CARTESIAN_POINT ( 'NONE',  ( 12.25000000000000711, 9.350000000011142731, -117.0215193718251641 ) ) ;
#125823=ORIENTED_EDGE ( 'NONE', *, *, #187662, .T. ) ;
#125958=LINE ( 'NONE', #11160, #528 ) ;
#126356=EDGE_CURVE ( 'NONE', #93005, #237169, #98783, .T. ) ;
#126392=DIRECTION ( 'NONE',  ( 1.000000000000000000, 0.000000000000000000, 0.000000000000000000 ) ) ;
#126409=CARTESIAN_POINT ( 'NONE',  ( 18.54999999999999716, 9.950000000011153034, -121.3500000000000938 ) ) ;
#126754=ORIENTED_EDGE ( 'NONE', *, *, #175210, .F. ) ;
#126872=CARTESIAN_POINT ( 'NONE',  ( -15.55912972643740488, 8.490870273573721150, -121.4500000000000313 ) ) ;
#126934=CARTESIAN_POINT ( 'NONE',  ( -15.39946565075090668, 9.389534562357859215, -116.1748093043900099 ) ) ;
#127257=CARTESIAN_POINT ( 'NONE',  ( -15.73854595235692244, 9.351413679112546617, -117.4803435675490135 ) ) ;
#127269=CARTESIAN_POINT ( 'NONE',  ( -16.93433913041102912, 10.00597842153509376, -121.4353654273952117 ) ) ;
#127334=ORIENTED_EDGE ( 'NONE', *, *, #94426, .T. ) ;
#127523=DIRECTION ( 'NONE',  ( -1.073024830501117725E-15, 0.000000000000000000, 1.000000000000000000 ) ) ;
#127788=( BOUNDED_CURVE ( )  B_SPLINE_CURVE ( 3, ( #227967, #108025, #49323, #208427 ),
 .UNSPECIFIED., .F., .F. ) 
 B_SPLINE_CURVE_WITH_KNOTS ( ( 4, 4 ),
 ( 0.000000000000000000, 1.570796326794896558 ),
 .UNSPECIFIED. ) 
 CURVE ( )  GEOMETRIC_REPRESENTATION_ITEM ( )  RATIONAL_B_SPLINE_CURVE ( ( 1.000000000000000000, 0.8047378541243649375, 0.8047378541243649375, 1.000000000000000000 ) ) 
 REPRESENTATION_ITEM ( '' )  );
#128221=CARTESIAN_POINT ( 'NONE',  ( -15.52965525596988172, 9.375538102059159939, -116.3698758809908753 ) ) ;
#128310=EDGE_LOOP ( 'NONE', ( #145187, #203607, #226099, #249395, #142513 ) ) ;
#128328=DIRECTION ( 'NONE',  ( -0.7071067811865456854, 0.7071067811865493491, 0.000000000000000000 ) ) ;
#128435=CARTESIAN_POINT ( 'NONE',  ( -16.94107738177414291, 10.01423928514777373, -121.4500000000000313 ) ) ;
#128541=CARTESIAN_POINT ( 'NONE',  ( -14.45422546970483957, 9.450602096099682825, -118.9438959630967219 ) ) ;
#128725=DIRECTION ( 'NONE',  ( 0.000000000000000000, 0.000000000000000000, -1.000000000000000000 ) ) ;
#128792=ORIENTED_EDGE ( 'NONE', *, *, #257486, .T. ) ;
#129065=ADVANCED_FACE ( 'NONE', ( #205029 ), #88944, .F. ) ;
#129268=DIRECTION ( 'NONE',  ( 1.000000000000000000, 0.000000000000000000, -0.000000000000000000 ) ) ;
#129349=EDGE_CURVE ( 'NONE', #47116, #135449, #32229, .T. ) ;
#129372=DIRECTION ( 'NONE',  ( -0.5932847527679298016, 0.8049926720990051576, 0.000000000000000000 ) ) ;
#129428=DIRECTION ( 'NONE',  ( 1.073024830501117725E-15, 0.000000000000000000, 1.000000000000000000 ) ) ;
#129649=ADVANCED_FACE ( 'NONE', ( #85409 ), #741, .T. ) ;
#129727=ORIENTED_EDGE ( 'NONE', *, *, #156590, .F. ) ;
#129850=CARTESIAN_POINT ( 'NONE',  ( -16.93658211146646408, 9.994108662352344297, -113.0957049300443487 ) ) ;
#129978=EDGE_CURVE ( 'NONE', #107983, #229722, #181175, .T. ) ;
#129982=ORIENTED_EDGE ( 'NONE', *, *, #14131, .F. ) ;
#130124=FACE_OUTER_BOUND ( 'NONE', #179349, .T. ) ;
#130512=AXIS2_PLACEMENT_3D ( 'NONE', #180238, #220641, #1570 ) ;
#130720=ORIENTED_EDGE ( 'NONE', *, *, #187472, .F. ) ;
#130850=CIRCLE ( 'NONE', #251467, 1.749999999999998002 ) ;
#130992=LINE ( 'NONE', #250919, #251613 ) ;
#131071=ADVANCED_FACE ( 'NONE', ( #253539 ), #176607, .F. ) ;
#131281=CIRCLE ( 'NONE', #164615, 14.20833333333333748 ) ;
#131283=CARTESIAN_POINT ( 'NONE',  ( -16.88783316861809780, 9.950000000011137047, -113.2522640419798279 ) ) ;
#131346=DIRECTION ( 'NONE',  ( 0.000000000000000000, 0.000000000000000000, 1.000000000000000000 ) ) ;
#131518=DIRECTION ( 'NONE',  ( 1.020425574104004196E-15, 1.210927747993693964E-31, 1.000000000000000000 ) ) ;
#131550=CARTESIAN_POINT ( 'NONE',  ( -23.25000000000000355, 11.75000000001113953, -109.7500000000000426 ) ) ;
#131712=CARTESIAN_POINT ( 'NONE',  ( -18.40000000000000213, 11.48667500176882861, -124.7500000000000284 ) ) ;
#132263=LINE ( 'NONE', #12344, #156240 ) ;
#132344=CIRCLE ( 'NONE', #86537, 0.1000000000000001305 ) ;
#132436=CARTESIAN_POINT ( 'NONE',  ( -16.93970660449832621, 10.01284139164672915, -113.0522817357944945 ) ) ;
#132577=FACE_OUTER_BOUND ( 'NONE', #257628, .T. ) ;
#132587=CARTESIAN_POINT ( 'NONE',  ( 15.51872946208854920, 9.376580978055097049, -118.1269462470119862 ) ) ;
#132789=EDGE_CURVE ( 'NONE', #67859, #189017, #112305, .T. ) ;
#133196=( BOUNDED_SURFACE ( )  B_SPLINE_SURFACE ( 3, 2, ( 
 ( #213378, #209540, #193838 ),
 ( #230387, #252500, #93429 ),
 ( #153469, #135115, #173032 ),
 ( #214665, #71336, #72619 ),
 ( #51718, #36052, #73913 ),
 ( #131283, #70055, #212120 ),
 ( #15206, #169163, #94717 ),
 ( #231687, #248665, #174316 ),
 ( #149590, #253779, #210824 ),
 ( #113011, #75189, #115568 ) ),
 .UNSPECIFIED., .F., .F., .F. ) 
 B_SPLINE_SURFACE_WITH_KNOTS ( ( 4, 2, 2, 2, 4 ),
 ( 3, 3 ),
 ( 0.002161241639767785133, 0.002579950749617447234, 0.002789305304542278284, 0.002893982582004694243, 0.002998659859467109768 ),
 ( 0.000000000000000000, 1.000000000000000000 ),
 .UNSPECIFIED. ) 
 GEOMETRIC_REPRESENTATION_ITEM ( )  RATIONAL_B_SPLINE_SURFACE ( (
 ( 1.000000000000000000, 0.7071067811864923947, 1.000000000000000000),
 ( 1.000000000000000000, 0.7632447400662122350, 1.000000000000000000),
 ( 1.000000000000000000, 0.8158073005111775577, 1.000000000000000000),
 ( 1.000000000000000000, 0.8906973462394580654, 1.000000000000000000),
 ( 1.000000000000000000, 0.9149408947800606873, 1.000000000000000000),
 ( 1.000000000000000000, 0.9493368785275470012, 1.000000000000000000),
 ( 1.000000000000000000, 0.9605194247155928178, 1.000000000000000000),
 ( 1.000000000000000000, 0.9803630264781846293, 1.000000000000000000),
 ( 1.000000000000000000, 0.9900844824270638167, 1.000000000000000000),
 ( 1.000000000000000000, 0.9894588281429246290, 1.000000000000000000) ) ) 
 REPRESENTATION_ITEM ( '' )  SURFACE ( )  );
#133341=EDGE_CURVE ( 'NONE', #245454, #141252, #75450, .T. ) ;
#133449=VECTOR ( 'NONE', #246556, 1000.000000000000000 ) ;
#133581=VERTEX_POINT ( 'NONE', #12594 ) ;
#133622=CARTESIAN_POINT ( 'NONE',  ( -16.87036670365548474, 9.989418819312801290, -121.4795601173020856 ) ) ;
#133642=DIRECTION ( 'NONE',  ( 1.186688945009010077E-16, -1.000000000000000000, -0.000000000000000000 ) ) ;
#133676=CARTESIAN_POINT ( 'NONE',  ( -21.64999999999999858, 9.350000000011133849, -109.7500000000000426 ) ) ;
#133913=CARTESIAN_POINT ( 'NONE',  ( -16.91049119928362643, 9.950000000011135270, -121.3817203931908750 ) ) ;
#133991=CARTESIAN_POINT ( 'NONE',  ( -12.25000000000000178, 9.350000000011139178, -117.2500000000000284 ) ) ;
#134038=DIRECTION ( 'NONE',  ( 1.000000000000000000, 0.000000000000000000, 0.000000000000000000 ) ) ;
#134082=CARTESIAN_POINT ( 'NONE',  ( -16.87331047859649757, 9.950000000011138823, -121.3500000000000369 ) ) ;
#134221=ORIENTED_EDGE ( 'NONE', *, *, #94426, .F. ) ;
#134335=EDGE_LOOP ( 'NONE', ( #147664, #48796, #97615, #163353 ) ) ;
#134495=VECTOR ( 'NONE', #215882, 1000.000000000000000 ) ;
#134498=ORIENTED_EDGE ( 'NONE', *, *, #216957, .F. ) ;
#134575=CARTESIAN_POINT ( 'NONE',  ( -16.89268316805465986, 9.951721813253337601, -121.3557524785455826 ) ) ;
#134606=CARTESIAN_POINT ( 'NONE',  ( -12.24999999999999289, 9.350000000011130297, -117.0185689574026213 ) ) ;
#134768=VECTOR ( 'NONE', #128328, 1000.000000000000000 ) ;
#134802=DIRECTION ( 'NONE',  ( 0.000000000000000000, -0.9553114395362780620, -0.2956011730205483912 ) ) ;
#134923=CARTESIAN_POINT ( 'NONE',  ( -18.37013991200266005, 11.49974761622313224, -124.7930230105171461 ) ) ;
#134971=CARTESIAN_POINT ( 'NONE',  ( -16.94309007106719633, 9.992226192581140864, -113.1057912825555292 ) ) ;
#135005=CIRCLE ( 'NONE', #168418, 0.1000000000000028644 ) ;
#135115=CARTESIAN_POINT ( 'NONE',  ( -16.89935556175728948, 9.950000000011010926, -113.6396763628857940 ) ) ;
#135127=CARTESIAN_POINT ( 'NONE',  ( 14.88075390448864965, 9.431689550535256927, -118.7792900322361049 ) ) ;
#135160=DIRECTION ( 'NONE',  ( 0.000000000000000000, 0.000000000000000000, 1.000000000000000000 ) ) ;
#135184=CARTESIAN_POINT ( 'NONE',  ( -16.94107738177415712, 10.01423928514777550, -113.0500000000000398 ) ) ;
#135376=DIRECTION ( 'NONE',  ( -1.020425574104004196E-15, 0.000000000000000000, 1.000000000000000000 ) ) ;
#135449=VERTEX_POINT ( 'NONE', #45986 ) ;
#135450=ORIENTED_EDGE ( 'NONE', *, *, #222613, .T. ) ;
#135620=LINE ( 'NONE', #36578, #56174 ) ;
#135911=ADVANCED_FACE ( 'NONE', ( #239273 ), #157190, .T. ) ;
#136006=CARTESIAN_POINT ( 'NONE',  ( -33.72168855820451938, 9.950000000011156587, -113.1499999999999773 ) ) ;
#136163=CIRCLE ( 'NONE', #111273, 0.9000000000000014655 ) ;
#136203=CARTESIAN_POINT ( 'NONE',  ( -17.27223548804798270, 10.34539739142601000, -122.6336061791826211 ) ) ;
#136241=AXIS2_PLACEMENT_3D ( 'NONE', #255711, #96647, #17170 ) ;
#136268=ORIENTED_EDGE ( 'NONE', *, *, #243745, .T. ) ;
#136343=CARTESIAN_POINT ( 'NONE',  ( -16.86757978335471719, 9.965650379045438712, -113.0980046531675356 ) ) ;
#136377=CYLINDRICAL_SURFACE ( 'NONE', #42283, 0.9000000000000014655 ) ;
#136556=ADVANCED_FACE ( 'NONE', ( #136621 ), #79209, .F. ) ;
#136621=FACE_OUTER_BOUND ( 'NONE', #183223, .T. ) ;
#136739=DIRECTION ( 'NONE',  ( -0.000000000000000000, 1.000000000000000000, 0.000000000000000000 ) ) ;
#136926=DIRECTION ( 'NONE',  ( -0.000000000000000000, 1.000000000000000000, -0.000000000000000000 ) ) ;
#137026=PRODUCT_DEFINITION_SHAPE ( 'NONE', 'NONE',  #171249 ) ;
#137237=EDGE_CURVE ( 'NONE', #71501, #44121, #234811, .T. ) ;
#137428=B_SPLINE_CURVE_WITH_KNOTS ( 'NONE', 3,
 ( #26276, #6696, #165803, #56074, #251733, #255527, #117363, #176078, #174814, #73131 ),
 .UNSPECIFIED., .F., .F.,
 ( 4, 3, 3, 4 ),
 ( 1.894194122894209342E-15, 3.877043167000115254E-05, 7.336897548477166022E-05, 7.659383120240389282E-05 ),
 .UNSPECIFIED. ) ;
#137502=CARTESIAN_POINT ( 'NONE',  ( -17.29838795458689660, 10.37154985796053097, -122.6047412826064829 ) ) ;
#137727=FILL_AREA_STYLE_COLOUR ( '', #106458 ) ;
#137732=VERTEX_POINT ( 'NONE', #203062 ) ;
#138013=CARTESIAN_POINT ( 'NONE',  ( 17.23472005113827876, 10.30788195451192379, -111.9534231399313597 ) ) ;
#138034=EDGE_CURVE ( 'NONE', #167339, #93005, #76376, .T. ) ;
#138124=ADVANCED_FACE ( 'NONE', ( #175523 ), #116809, .F. ) ;
#138129=ORIENTED_EDGE ( 'NONE', *, *, #199194, .F. ) ;
#138175=VECTOR ( 'NONE', #230980, 1000.000000000000000 ) ;
#138239=VERTEX_POINT ( 'NONE', #247010 ) ;
#138275=CARTESIAN_POINT ( 'NONE',  ( -16.78493832629887450, 9.945835743215301505, -113.1639490191042796 ) ) ;
#138325=LINE ( 'NONE', #41847, #187148 ) ;
#138377=CARTESIAN_POINT ( 'NONE',  ( -16.97683809663752186, 9.950000000011137047, -120.5976359818037196 ) ) ;
#138492=DIRECTION ( 'NONE',  ( -1.000000000000000000, 0.000000000000000000, 0.000000000000000000 ) ) ;
#138667=CARTESIAN_POINT ( 'NONE',  ( -16.77683809663752257, 9.945835743215301505, -113.1639490191042512 ) ) ;
#138908=ORIENTED_EDGE ( 'NONE', *, *, #87589, .T. ) ;
#139118=CARTESIAN_POINT ( 'NONE',  ( -17.04761207306819060, 10.02645087340892438, -113.1500000000000483 ) ) ;
#139419=CARTESIAN_POINT ( 'NONE',  ( -18.35663730107557257, 11.47390742652235573, -109.7500000000000426 ) ) ;
#139461=CARTESIAN_POINT ( 'NONE',  ( -16.97683809663752186, 9.950000000011138823, -113.9023640181965220 ) ) ;
#139561=VECTOR ( 'NONE', #240853, 1000.000000000000000 ) ;
#139633=DIRECTION ( 'NONE',  ( -1.000000000000000000, 0.000000000000000000, 0.000000000000000000 ) ) ;
#139660=CARTESIAN_POINT ( 'NONE',  ( -16.80891096016338437, 9.950000000011137047, -121.3676628072671235 ) ) ;
#140210=CARTESIAN_POINT ( 'NONE',  ( 23.04999999999999716, 8.822561741677553471, -113.1500000000000483 ) ) ;
#140602=CARTESIAN_POINT ( 'NONE',  ( -21.65000000000000213, 7.250000000011138646, -113.1500000000000341 ) ) ;
#140631=DIRECTION ( 'NONE',  ( -0.000000000000000000, 1.000000000000000000, 0.000000000000000000 ) ) ;
#140732=CARTESIAN_POINT ( 'NONE',  ( -16.93415306273742260, 9.995622260023669270, -121.4100569423604412 ) ) ;
#140916=CARTESIAN_POINT ( 'NONE',  ( -16.77828822508139694, 9.946229374931901290, -113.1626282513739881 ) ) ;
#141163=EDGE_CURVE ( 'NONE', #185216, #40045, #251188, .T. ) ;
#141252=VERTEX_POINT ( 'NONE', #219127 ) ;
#141271=CARTESIAN_POINT ( 'NONE',  ( -33.72168855820452649, 11.47316190337362585, -109.7500000000000284 ) ) ;
#141550=AXIS2_PLACEMENT_3D ( 'NONE', #103263, #5443, #244074 ) ;
#141671=CARTESIAN_POINT ( 'NONE',  ( -16.81453563122428463, 9.939100205448109904, -121.2882586606453401 ) ) ;
#142125=EDGE_LOOP ( 'NONE', ( #89044, #115160, #29775, #231345, #6435, #227904, #119004, #4244, #152178 ) ) ;
#142189=CARTESIAN_POINT ( 'NONE',  ( -16.81744102076749314, 9.950000000011142376, -113.1500000000000341 ) ) ;
#142435=AXIS2_PLACEMENT_3D ( 'NONE', #44210, #65039, #102858 ) ;
#142513=ORIENTED_EDGE ( 'NONE', *, *, #112045, .T. ) ;
#142585=ORIENTED_EDGE ( 'NONE', *, *, #197405, .T. ) ;
#142746=EDGE_LOOP ( 'NONE', ( #214753, #248328, #204255, #201274 ) ) ;
#142798=CARTESIAN_POINT ( 'NONE',  ( 14.22821877134046709, 9.456028260519074635, -115.5111980350658030 ) ) ;
#142847=VECTOR ( 'NONE', #210498, 1000.000000000000000 ) ;
#142989=FACE_OUTER_BOUND ( 'NONE', #65164, .T. ) ;
#143077=VECTOR ( 'NONE', #198463, 1000.000000000000000 ) ;
#143132=AXIS2_PLACEMENT_3D ( 'NONE', #40450, #44273, #45548 ) ;
#143389=DIRECTION ( 'NONE',  ( 1.000000000000000000, 1.186688945009009831E-16, 0.000000000000000000 ) ) ;
#143405=CARTESIAN_POINT ( 'NONE',  ( -18.40000000000000213, 5.650000000011139001, -113.1500000000000341 ) ) ;
#143431=DIRECTION ( 'NONE',  ( -1.073024830501117725E-15, -0.000000000000000000, -1.000000000000000000 ) ) ;
#143597=VECTOR ( 'NONE', #131518, 1000.000000000000000 ) ;
#143847=CARTESIAN_POINT ( 'NONE',  ( 18.39999999999999503, 11.47316190337363828, -121.3500000000000369 ) ) ;
#144012=EDGE_CURVE ( 'NONE', #112606, #168680, #64905, .T. ) ;
#144088=ORIENTED_EDGE ( 'NONE', *, *, #133341, .T. ) ;
#144089=CARTESIAN_POINT ( 'NONE',  ( 12.47034474403012183, 9.375538102059159939, -116.3698758809908611 ) ) ;
#144107=DIRECTION ( 'NONE',  ( 0.000000000000000000, 0.000000000000000000, -1.000000000000000000 ) ) ;
#144119=CARTESIAN_POINT ( 'NONE',  ( -16.92973740335348509, 9.992503814478576274, -121.4060590352024462 ) ) ;
#144120=EDGE_CURVE ( 'NONE', #233466, #221470, #71356, .T. ) ;
#144229=CARTESIAN_POINT ( 'NONE',  ( -12.33960340485503338, 9.360749169926259938, -117.8145701406072874 ) ) ;
#144356=CARTESIAN_POINT ( 'NONE',  ( -23.25000000000000355, 11.75000000001113953, -109.7500000000000426 ) ) ;
#144603=CARTESIAN_POINT ( 'NONE',  ( -16.87851181299898684, 9.950042924018893231, -113.1498564846331192 ) ) ;
#144675=DIRECTION ( 'NONE',  ( 1.000000000000000000, 0.000000000000000000, -1.020425574104004196E-15 ) ) ;
#144738=CARTESIAN_POINT ( 'NONE',  ( -16.80438519320023616, 9.949779096479501206, -113.1507382809213027 ) ) ;
#144841=ORIENTED_EDGE ( 'NONE', *, *, #224707, .F. ) ;
#145051=CIRCLE ( 'NONE', #32687, 0.9000000000000014655 ) ;
#145091=EDGE_LOOP ( 'NONE', ( #75934, #91612, #251084, #125823, #166286, #171642 ) ) ;
#145123=DIRECTION ( 'NONE',  ( 1.000000000000000000, 0.000000000000000000, 1.073024830501117725E-15 ) ) ;
#145187=ORIENTED_EDGE ( 'NONE', *, *, #176456, .F. ) ;
#145372=CARTESIAN_POINT ( 'NONE',  ( -18.40000000000000213, 5.650000000011139001, -113.1500000000000341 ) ) ;
#145523=CARTESIAN_POINT ( 'NONE',  ( -12.26136940704871670, 9.351403174152810749, -117.4795304368385018 ) ) ;
#145576=CARTESIAN_POINT ( 'NONE',  ( -20.65000000000000568, 5.650000000011139001, -113.1500000000000341 ) ) ;
#145735=VERTEX_POINT ( 'NONE', #38370 ) ;
#145793=STYLED_ITEM ( 'NONE', ( #100224 ), #107560 ) ;
#145803=CARTESIAN_POINT ( 'NONE',  ( -18.40000000000000213, 11.47316190337362940, -113.1085786437627263 ) ) ;
#146003=ORIENTED_EDGE ( 'NONE', *, *, #89025, .T. ) ;
#146351=DIRECTION ( 'NONE',  ( -0.000000000000000000, 1.000000000000000000, -0.000000000000000000 ) ) ;
#146573=ORIENTED_EDGE ( 'NONE', *, *, #60124, .F. ) ;
#146607=DIRECTION ( 'NONE',  ( 0.000000000000000000, 1.000000000000000000, 0.000000000000000000 ) ) ;
#146677=ADVANCED_FACE ( 'NONE', ( #183701 ), #241119, .T. ) ;
#146681=CARTESIAN_POINT ( 'NONE',  ( -16.86445178670638612, 9.962211629127159185, -121.3907774381173681 ) ) ;
#146716=CARTESIAN_POINT ( 'NONE',  ( -16.89081410710458542, 9.951318529858268036, -121.3544059198363954 ) ) ;
#146723=CARTESIAN_POINT ( 'NONE',  ( -16.84421487269769813, 9.950000000011140600, -113.1695021224450386 ) ) ;
#146777=AXIS2_PLACEMENT_3D ( 'NONE', #182655, #238763, #139633 ) ;
#146785=VERTEX_POINT ( 'NONE', #51856 ) ;
#146795=CARTESIAN_POINT ( 'NONE',  ( -15.39126916658602973, 9.389571634557565716, -118.3176407123691689 ) ) ;
#147116=DIRECTION ( 'NONE',  ( -1.020425574104004196E-15, -1.210927747993693964E-31, -1.000000000000000000 ) ) ;
#147372=ORIENTED_EDGE ( 'NONE', *, *, #60124, .T. ) ;
#147424=B_SPLINE_CURVE_WITH_KNOTS ( 'NONE', 3,
 ( #179394, #121971, #256268, #77685, #704, #80231, #159828, #3281, #82799, #239352 ),
 .UNSPECIFIED., .F., .F.,
 ( 4, 3, 3, 4 ),
 ( 7.632826238681696029E-06, 4.756916949875625587E-05, 9.484459048150268483E-05, 0.0001435500935099809469 ),
 .UNSPECIFIED. ) ;
#147453=EDGE_CURVE ( 'NONE', #141252, #162376, #71600, .T. ) ;
#147664=ORIENTED_EDGE ( 'NONE', *, *, #110111, .F. ) ;
#147831=LINE ( 'NONE', #48705, #34601 ) ;
#148010=( GEOMETRIC_REPRESENTATION_CONTEXT ( 3 ) GLOBAL_UNCERTAINTY_ASSIGNED_CONTEXT ( ( #73822 ) ) GLOBAL_UNIT_ASSIGNED_CONTEXT ( ( #175605, #116900, #156058 ) ) REPRESENTATION_CONTEXT ( 'NONE', 'WORKASPACE' ) );
#148037=CARTESIAN_POINT ( 'NONE',  ( -16.87665923198281348, 9.950000000011138823, -121.3500000000000369 ) ) ;
#148119=CARTESIAN_POINT ( 'NONE',  ( -16.93589915522259304, 10.00862525870701170, -121.4405601019603438 ) ) ;
#148349=EDGE_CURVE ( 'NONE', #47116, #167911, #157550, .T. ) ;
#148650=VECTOR ( 'NONE', #140631, 1000.000000000000000 ) ;
#148733=ADVANCED_FACE ( 'NONE', ( #216582 ), #18383, .F. ) ;
#148803=VECTOR ( 'NONE', #16515, 1000.000000000000000 ) ;
#148813=ORIENTED_EDGE ( 'NONE', *, *, #25120, .F. ) ;
#148819=FACE_OUTER_BOUND ( 'NONE', #82705, .T. ) ;
#148852=EDGE_CURVE ( 'NONE', #75516, #237169, #176847, .T. ) ;
#148864=VECTOR ( 'NONE', #27694, 999.9999999999998863 ) ;
#148916=CARTESIAN_POINT ( 'NONE',  ( -16.94107738177414291, 10.01423928514777373, -121.4500000000000313 ) ) ;
#149081=CARTESIAN_POINT ( 'NONE',  ( -12.29659703204451660, 9.355888454513701546, -116.7886428967780290 ) ) ;
#149255=LINE ( 'NONE', #145372, #213607 ) ;
#149410=CARTESIAN_POINT ( 'NONE',  ( -14.22969084473440304, 9.456007326080463571, -118.9886334941467823 ) ) ;
#149417=EDGE_CURVE ( 'NONE', #40045, #108024, #132344, .T. ) ;
#149590=CARTESIAN_POINT ( 'NONE',  ( -16.80891096016346964, 9.950000000011137047, -113.1323371927329333 ) ) ;
#149601=CARTESIAN_POINT ( 'NONE',  ( 15.39170923737819585, 9.389529397477893724, -118.3171079128937464 ) ) ;
#149653=DIRECTION ( 'NONE',  ( 0.000000000000000000, -1.000000000000000000, 0.000000000000000000 ) ) ;
#149768=ADVANCED_FACE ( 'NONE', ( #54958 ), #36742, .F. ) ;
#150046=AXIS2_PLACEMENT_3D ( 'NONE', #74983, #133642, #154530 ) ;
#150101=B_SPLINE_CURVE_WITH_KNOTS ( 'NONE', 3,
 ( #142189, #240018, #144738, #63942, #61368, #203456, #122651, #24844, #164336, #140916, #221702, #202169, #121387 ),
 .UNSPECIFIED., .F., .F.,
 ( 4, 3, 3, 3, 4 ),
 ( 1.084999851846394431E-16, 1.946463881814305957E-05, 3.922356109944007726E-05, 4.215060953238855979E-05, 4.415117091092329025E-05 ),
 .UNSPECIFIED. ) ;
#150175=DIRECTION ( 'NONE',  ( 0.000000000000000000, -1.000000000000000000, 0.000000000000000000 ) ) ;
#150182=LINE ( 'NONE', #206294, #148864 ) ;
#150358=CARTESIAN_POINT ( 'NONE',  ( -13.12432614554022869, 9.430764995433476017, -115.7305373947504989 ) ) ;
#150600=ORIENTED_EDGE ( 'NONE', *, *, #105877, .T. ) ;
#150688=ORIENTED_EDGE ( 'NONE', *, *, #242167, .T. ) ;
#150693=ORIENTED_EDGE ( 'NONE', *, *, #223346, .F. ) ;
#150801=VERTEX_POINT ( 'NONE', #30342 ) ;
#150833=ORIENTED_EDGE ( 'NONE', *, *, #159749, .T. ) ;
#150947=ORIENTED_EDGE ( 'NONE', *, *, #221765, .F. ) ;
#150984=CARTESIAN_POINT ( 'NONE',  ( -16.87683809663752399, 9.850000000011144508, -120.5976359818037338 ) ) ;
#151035=ORIENTED_EDGE ( 'NONE', *, *, #121542, .F. ) ;
#151173=CARTESIAN_POINT ( 'NONE',  ( -16.87683809663752399, 9.950000000011142376, -113.1500000000000341 ) ) ;
#151469=( BOUNDED_SURFACE ( )  B_SPLINE_SURFACE ( 3, 2, ( 
 ( #54379, #133913, #193909 ),
 ( #94788, #234294, #36123 ),
 ( #62090, #162486, #3374 ),
 ( #205428, #81606, #26838 ) ),
 .UNSPECIFIED., .F., .F., .F. ) 
 B_SPLINE_SURFACE_WITH_KNOTS ( ( 4, 4 ),
 ( 3, 3 ),
 ( 3.658908243880847788, 4.712388980384689674 ),
 ( 0.000000000000000000, 1.000000000000000000 ),
 .UNSPECIFIED. ) 
 GEOMETRIC_REPRESENTATION_ITEM ( )  RATIONAL_B_SPLINE_SURFACE ( (
 ( 1.000000000000000000, 0.8984936768950536612, 1.000000000000000000),
 ( 1.000000000000000000, 0.8646876308615781825, 1.000000000000000000),
 ( 1.000000000000000000, 0.7953136715913041721, 1.000000000000000000),
 ( 1.000000000000000000, 0.7071067811865475727, 1.000000000000000000) ) ) 
 REPRESENTATION_ITEM ( '' )  SURFACE ( )  );
#151636=FACE_OUTER_BOUND ( 'NONE', #245798, .T. ) ;
#151659=CARTESIAN_POINT ( 'NONE',  ( 20.99999999999999645, 9.750000000011137757, -121.3500000000000227 ) ) ;
#151872=SHAPE_REPRESENTATION ( 'Snap Open Cable Crossbars 4', ( #2425 ), #252228 ) ;
#151890=ORIENTED_EDGE ( 'NONE', *, *, #147453, .T. ) ;
#152173=CARTESIAN_POINT ( 'NONE',  ( 12.25000000000000000, 9.350000000011140955, -117.2500000000000284 ) ) ;
#152178=ORIENTED_EDGE ( 'NONE', *, *, #125615, .F. ) ;
#152317=CARTESIAN_POINT ( 'NONE',  ( -33.72168855820451938, 9.950000000011156587, -121.3500000000000938 ) ) ;
#152572=ORIENTED_EDGE ( 'NONE', *, *, #34208, .T. ) ;
#152587=ORIENTED_EDGE ( 'NONE', *, *, #228009, .F. ) ;
#152686=DIRECTION ( 'NONE',  ( 0.000000000000000000, -1.000000000000000000, 0.000000000000000000 ) ) ;
#152863=CARTESIAN_POINT ( 'NONE',  ( -16.84419801905645997, 9.950000000011140600, -121.3305101537780075 ) ) ;
#152982=CARTESIAN_POINT ( 'NONE',  ( 21.72449340488910607, 10.28395627750226815, -121.3500000000000227 ) ) ;
#153029=ORIENTED_EDGE ( 'NONE', *, *, #1985, .T. ) ;
#153070=VECTOR ( 'NONE', #67824, 1000.000000000000000 ) ;
#153243=CARTESIAN_POINT ( 'NONE',  ( 18.39999999999997371, 11.47316190337362940, -124.7500000000000426 ) ) ;
#153366=DIRECTION ( 'NONE',  ( -0.000000000000000000, -0.000000000000000000, -1.000000000000000000 ) ) ;
#153469=CARTESIAN_POINT ( 'NONE',  ( -16.96982749440708460, 9.950000000011137047, -113.6247784088119062 ) ) ;
#153513=CARTESIAN_POINT ( 'NONE',  ( 0.000000000000000000, 0.000000000000000000, 0.000000000000000000 ) ) ;
#153534=CARTESIAN_POINT ( 'NONE',  ( -16.92973740335373734, 9.992503814478400415, -113.0939409647979943 ) ) ;
#154017=CARTESIAN_POINT ( 'NONE',  ( -23.25000000000000355, 11.75000000001113953, -121.3500000000000369 ) ) ;
#154053=CARTESIAN_POINT ( 'NONE',  ( -20.65000000000000568, 5.650000000011139001, -121.3500000000000369 ) ) ;
#154095=ORIENTED_EDGE ( 'NONE', *, *, #252443, .F. ) ;
#154159=EDGE_CURVE ( 'NONE', #157238, #189017, #63557, .T. ) ;
#154306=CARTESIAN_POINT ( 'NONE',  ( -20.65000000000000568, 7.250000000011138646, -121.3500000000000369 ) ) ;
#154319=DIRECTION ( 'NONE',  ( -1.000000000000000000, 0.000000000000000000, 0.000000000000000000 ) ) ;
#154492=DIRECTION ( 'NONE',  ( -1.000000000000000000, -1.646408749285562691E-14, 0.000000000000000000 ) ) ;
#154530=DIRECTION ( 'NONE',  ( 1.000000000000000000, 0.000000000000000000, 0.000000000000000000 ) ) ;
#154645=CARTESIAN_POINT ( 'NONE',  ( -17.11825945287482753, 9.950000000011138823, -113.2500000000000284 ) ) ;
#154738=CARTESIAN_POINT ( 'NONE',  ( 15.31784899511109899, 9.396630376328872103, -118.4070573928183165 ) ) ;
#154769=SURFACE_STYLE_USAGE ( .BOTH. , #97293 ) ;
#154953=CARTESIAN_POINT ( 'NONE',  ( 21.13736287352038445, 8.046642376395153562, -109.7500000000000426 ) ) ;
#155057=DIRECTION ( 'NONE',  ( 1.000000000000000000, 0.000000000000000000, 0.000000000000000000 ) ) ;
#155199=CARTESIAN_POINT ( 'NONE',  ( -20.65000000000000568, 7.250000000011138646, -121.3500000000000369 ) ) ;
#155249=DIRECTION ( 'NONE',  ( -1.652117596168391700E-15, -1.000000000000000000, 0.000000000000000000 ) ) ;
#155720=ORIENTED_EDGE ( 'NONE', *, *, #191929, .F. ) ;
#155722=ORIENTED_EDGE ( 'NONE', *, *, #144120, .F. ) ;
#156058=( NAMED_UNIT ( * ) SI_UNIT ( $, .STERADIAN. ) SOLID_ANGLE_UNIT ( ) );
#156084=CARTESIAN_POINT ( 'NONE',  ( -16.90202395485750841, 9.965944544562109542, -113.0969862787403457 ) ) ;
#156240=VECTOR ( 'NONE', #94414, 1000.000000000000000 ) ;
#156451=ORIENTED_EDGE ( 'NONE', *, *, #60134, .T. ) ;
#156590=EDGE_CURVE ( 'NONE', #245594, #228258, #196899, .T. ) ;
#156707=ORIENTED_EDGE ( 'NONE', *, *, #34208, .F. ) ;
#157115=PRODUCT_DEFINITION_FORMATION_WITH_SPECIFIED_SOURCE ( 'ANY', '', #122620, .NOT_KNOWN. ) ;
#157151=AXIS2_PLACEMENT_3D ( 'NONE', #58425, #192846, #18039 ) ;
#157190=PLANE ( 'NONE',  #105934 ) ;
#157238=VERTEX_POINT ( 'NONE', #66060 ) ;
#157247=CARTESIAN_POINT ( 'NONE',  ( 23.24999999999999645, 11.75000000001113953, -109.7500000000000426 ) ) ;
#157256=CARTESIAN_POINT ( 'NONE',  ( -16.86337532320262156, 9.979967204235514089, -113.0510755310172328 ) ) ;
#157304=VECTOR ( 'NONE', #197579, 1000.000000000000000 ) ;
#157550=B_SPLINE_CURVE_WITH_KNOTS ( 'NONE', 3,
 ( #194783, #175240, #53954, #56503, #255957, #215589, #12290 ),
 .UNSPECIFIED., .F., .F.,
 ( 4, 3, 4 ),
 ( 0.000000000000000000, 3.882884552234470657E-05, 5.798605692158470456E-05 ),
 .UNSPECIFIED. ) ;
#157641=CARTESIAN_POINT ( 'NONE',  ( -21.65000000000000213, 7.250000000011139534, -113.1500000000000341 ) ) ;
#158013=CARTESIAN_POINT ( 'NONE',  ( -16.87683809663752399, 9.950000000011137047, -120.5976359818037196 ) ) ;
#158146=VECTOR ( 'NONE', #158917, 1000.000000000000000 ) ;
#158164=CARTESIAN_POINT ( 'NONE',  ( 20.99999999999999645, 9.750000000011137757, -121.3500000000000227 ) ) ;
#158495=LINE ( 'NONE', #39831, #157304 ) ;
#158747=VECTOR ( 'NONE', #63807, 1000.000000000000000 ) ;
#158771=CARTESIAN_POINT ( 'NONE',  ( -21.64999999999999858, 9.350000000011133849, -121.3500000000000369 ) ) ;
#158809=B_SPLINE_CURVE_WITH_KNOTS ( 'NONE', 3,
 ( #97715, #19509, #59878, #139419, #176028, #80730, #218967 ),
 .UNSPECIFIED., .F., .F.,
 ( 4, 3, 4 ),
 ( 0.000000000000000000, 4.520325912680675046E-05, 5.794988040901435228E-05 ),
 .UNSPECIFIED. ) ;
#158917=DIRECTION ( 'NONE',  ( 1.000000000000000000, 0.000000000000000000, 0.000000000000000000 ) ) ;
#158978=SURFACE_STYLE_USAGE ( .BOTH. , #79390 ) ;
#159110=LINE ( 'NONE', #238623, #174171 ) ;
#159176=CARTESIAN_POINT ( 'NONE',  ( -16.83794237512074332, 9.926359221118628895, -113.3035421586989884 ) ) ;
#159253=VECTOR ( 'NONE', #138492, 1000.000000000000000 ) ;
#159527=LINE ( 'NONE', #21317, #114719 ) ;
#159749=EDGE_CURVE ( 'NONE', #55172, #162005, #67525, .T. ) ;
#159828=CARTESIAN_POINT ( 'NONE',  ( -16.86379686415369150, 9.975217759264314310, -121.4333898890903214 ) ) ;
#159850=DIRECTION ( 'NONE',  ( -0.000000000000000000, -0.000000000000000000, -1.000000000000000000 ) ) ;
#159859=CYLINDRICAL_SURFACE ( 'NONE', #35254, 14.30833333333335311 ) ;
#159997=ADVANCED_FACE ( 'NONE', ( #75261 ), #151469, .T. ) ;
#160145=VECTOR ( 'NONE', #155249, 1000.000000000000000 ) ;
#160306=CARTESIAN_POINT ( 'NONE',  ( 21.13736287352038445, 8.046642376395153562, -121.3500000000000227 ) ) ;
#160329=CARTESIAN_POINT ( 'NONE',  ( -16.93234230245721861, 9.998107370558241058, -121.4176902816662817 ) ) ;
#160422=FACE_OUTER_BOUND ( 'NONE', #199262, .T. ) ;
#160776=VERTEX_POINT ( 'NONE', #83575 ) ;
#161174=DIRECTION ( 'NONE',  ( 1.000000000000000000, 1.186688945009010077E-16, 0.000000000000000000 ) ) ;
#161307=CARTESIAN_POINT ( 'NONE',  ( -16.98495255085918032, 10.00556436600591681, -113.1346172062205397 ) ) ;
#161406=DIRECTION ( 'NONE',  ( -0.000000000000000000, -0.000000000000000000, -1.000000000000000000 ) ) ;
#161627=SHAPE_DEFINITION_REPRESENTATION ( #137026, #151872 ) ;
#161641=CARTESIAN_POINT ( 'NONE',  ( 12.25000000000000000, 9.850000000011137402, -117.2500000000000284 ) ) ;
#161938=PLANE ( 'NONE',  #11368 ) ;
#161940=DIRECTION ( 'NONE',  ( 0.000000000000000000, 0.000000000000000000, -1.000000000000000000 ) ) ;
#162005=VERTEX_POINT ( 'NONE', #114471 ) ;
#162161=ORIENTED_EDGE ( 'NONE', *, *, #1280, .T. ) ;
#162352=VERTEX_POINT ( 'NONE', #223202 ) ;
#162376=VERTEX_POINT ( 'NONE', #66716 ) ;
#162437=APPLICATION_CONTEXT ( 'automotive_design' ) ;
#162486=CARTESIAN_POINT ( 'NONE',  ( -17.05016517656263275, 9.950000000011140600, -121.3273020039994634 ) ) ;
#162517=ORIENTED_EDGE ( 'NONE', *, *, #76590, .T. ) ;
#162725=DIRECTION ( 'NONE',  ( 0.000000000000000000, 0.000000000000000000, -1.000000000000000000 ) ) ;
#162936=( BOUNDED_SURFACE ( )  B_SPLINE_SURFACE ( 3, 2, ( 
 ( #191591, #109435, #170766 ),
 ( #52026, #212421, #169472 ),
 ( #10372, #32524, #11657 ),
 ( #194147, #15512, #248979 ) ),
 .UNSPECIFIED., .F., .F., .F. ) 
 B_SPLINE_SURFACE_WITH_KNOTS ( ( 4, 4 ),
 ( 3, 3 ),
 ( 5.727910411845712702, 5.983100554402349225 ),
 ( 0.000000000000000000, 1.000000000000000000 ),
 .UNSPECIFIED. ) 
 GEOMETRIC_REPRESENTATION_ITEM ( )  RATIONAL_B_SPLINE_SURFACE ( (
 ( 1.000000000000000000, 0.8946697475932183785, 1.000000000000000000),
 ( 1.000000000000000000, 0.9035312726220445789, 1.000000000000000000),
 ( 1.000000000000000000, 0.9104333467450315132, 1.000000000000000000),
 ( 1.000000000000000000, 0.9152888060719349683, 1.000000000000000000) ) ) 
 REPRESENTATION_ITEM ( '' )  SURFACE ( )  );
#162947=CARTESIAN_POINT ( 'NONE',  ( -21.65000000000000213, 7.250000000011138646, -109.7500000000000426 ) ) ;
#163086=VERTEX_POINT ( 'NONE', #256522 ) ;
#163095=DIRECTION ( 'NONE',  ( 0.000000000000000000, -1.000000000000000000, 0.000000000000000000 ) ) ;
#163123=CARTESIAN_POINT ( 'NONE',  ( -16.93710578446422943, 9.950000000011137047, -121.0811960162006926 ) ) ;
#163215=DIRECTION ( 'NONE',  ( 1.000000000000000000, 0.000000000000000000, 0.000000000000000000 ) ) ;
#163233=ORIENTED_EDGE ( 'NONE', *, *, #113998, .T. ) ;
#163235=CARTESIAN_POINT ( 'NONE',  ( -21.65000000000000213, 9.950000000011138823, -113.2500000000000284 ) ) ;
#163292=EDGE_LOOP ( 'NONE', ( #13396, #61393, #228266, #134221 ) ) ;
#163353=ORIENTED_EDGE ( 'NONE', *, *, #215736, .F. ) ;
#163363=ADVANCED_FACE ( 'NONE', ( #32121 ), #191200, .F. ) ;
#163379=AXIS2_PLACEMENT_3D ( 'NONE', #231984, #7792, #112030 ) ;
#163733=SHAPE_REPRESENTATION_RELATIONSHIP ( 'NONE' , 'NONE' ,  #151872, #85670 ) ;
#164076=PLANE ( 'NONE',  #5947 ) ;
#164078=ORIENTED_EDGE ( 'NONE', *, *, #125000, .T. ) ;
#164320=EDGE_CURVE ( 'NONE', #55464, #199951, #203068, .T. ) ;
#164336=CARTESIAN_POINT ( 'NONE',  ( -16.77902162784673834, 9.946419257218996890, -113.1619912440693838 ) ) ;
#164615=AXIS2_PLACEMENT_3D ( 'NONE', #48809, #207914, #146607 ) ;
#164645=CIRCLE ( 'NONE', #31398, 1.749999999999999778 ) ;
#164657=ORIENTED_EDGE ( 'NONE', *, *, #175616, .F. ) ;
#165101=CARTESIAN_POINT ( 'NONE',  ( -14.77538296656415007, 9.436662931810239741, -118.8230367322948808 ) ) ;
#165149=EDGE_LOOP ( 'NONE', ( #206139, #255388, #9983 ) ) ;
#165253=LINE ( 'NONE', #247349, #61636 ) ;
#165485=LINE ( 'NONE', #245006, #158747 ) ;
#165578=CARTESIAN_POINT ( 'NONE',  ( -17.04295772865494740, 10.02489942527117783, -113.1500000000000483 ) ) ;
#165803=CARTESIAN_POINT ( 'NONE',  ( -16.91247567987037570, 9.959082683680399839, -113.1287244585373770 ) ) ;
#165959=CARTESIAN_POINT ( 'NONE',  ( 21.72449340488910252, 10.28395627750227526, -109.7500000000000426 ) ) ;
#166286=ORIENTED_EDGE ( 'NONE', *, *, #1985, .F. ) ;
#166315=CARTESIAN_POINT ( 'NONE',  ( -16.91256925476569251, 9.985731158139330432, -121.4676424890052999 ) ) ;
#166346=CARTESIAN_POINT ( 'NONE',  ( -16.88005004766534967, 9.950100503332199864, -121.3503361119487920 ) ) ;
#166375=ORIENTED_EDGE ( 'NONE', *, *, #124916, .F. ) ;
#166416=CARTESIAN_POINT ( 'NONE',  ( -12.25000000000000355, 9.350000000011135626, -117.3657431672739619 ) ) ;
#166789=CARTESIAN_POINT ( 'NONE',  ( -16.87331047859651179, 9.950000000011142376, -113.1500000000000341 ) ) ;
#167086=ADVANCED_FACE ( 'NONE', ( #102778 ), #164076, .F. ) ;
#167339=VERTEX_POINT ( 'NONE', #236870 ) ;
#167370=CARTESIAN_POINT ( 'NONE',  ( -14.23072895065543086, 9.455987233623901034, -115.5115311668978961 ) ) ;
#167541=LINE ( 'NONE', #48841, #142847 ) ;
#167557=CARTESIAN_POINT ( 'NONE',  ( 12.60053434924909865, 9.389534562357859215, -116.1748093043900099 ) ) ;
#167584=CARTESIAN_POINT ( 'NONE',  ( -16.92570016628983254, 9.958788957751014692, -121.3793493299610446 ) ) ;
#167911=VERTEX_POINT ( 'NONE', #131712 ) ;
#167969=CIRCLE ( 'NONE', #130512, 1.749999999999999778 ) ;
#168103=VERTEX_POINT ( 'NONE', #121173 ) ;
#168418=AXIS2_PLACEMENT_3D ( 'NONE', #9312, #129268, #250482 ) ;
#168513=VECTOR ( 'NONE', #153366, 1000.000000000000000 ) ;
#168542=EDGE_CURVE ( 'NONE', #230044, #46173, #238190, .T. ) ;
#168655=CARTESIAN_POINT ( 'NONE',  ( 18.39999999999999503, 5.650000000011139001, -113.1500000000000341 ) ) ;
#168680=VERTEX_POINT ( 'NONE', #222463 ) ;
#168896=MECHANICAL_DESIGN_GEOMETRIC_PRESENTATION_REPRESENTATION('',(#10648),#148010);
#168898=VECTOR ( 'NONE', #172009, 1000.000000000000000 ) ;
#168991=CARTESIAN_POINT ( 'NONE',  ( -14.11361717019515893, 9.457426452500060421, -119.0000418684000607 ) ) ;
#169163=CARTESIAN_POINT ( 'NONE',  ( -16.84793658983433318, 9.950000000011138823, -113.2336466778105404 ) ) ;
#169364=DIRECTION ( 'NONE',  ( 0.2834754621636439431, -0.2834754621636535465, -0.9161240771326838450 ) ) ;
#169365=CARTESIAN_POINT ( 'NONE',  ( -16.88219499860498374, 9.950206425438743452, -113.1493096901073443 ) ) ;
#169472=CARTESIAN_POINT ( 'NONE',  ( -17.73285935861322216, 10.85798180380187183, -110.7414381902193270 ) ) ;
#169494=ORIENTED_EDGE ( 'NONE', *, *, #41269, .T. ) ;
#170214=DIRECTION ( 'NONE',  ( -0.000000000000000000, -0.000000000000000000, -1.000000000000000000 ) ) ;
#170236=ORIENTED_EDGE ( 'NONE', *, *, #26071, .T. ) ;
#170478=CARTESIAN_POINT ( 'NONE',  ( 12.30626653967340900, 9.356790025057035720, -117.7048265086139338 ) ) ;
#170766=CARTESIAN_POINT ( 'NONE',  ( -18.37013991200266005, 11.49974761622312691, -109.7069769894829250 ) ) ;
#170893=AXIS2_PLACEMENT_3D ( 'NONE', #12555, #231590, #112918 ) ;
#170943=CARTESIAN_POINT ( 'NONE',  ( -18.40000000000000213, 11.47316190337362762, -113.0500000000000398 ) ) ;
#171017=CARTESIAN_POINT ( 'NONE',  ( 20.73486653747088582, 7.250000000011182166, -109.7500000000000426 ) ) ;
#171085=ORIENTED_EDGE ( 'NONE', *, *, #30834, .T. ) ;
#171249=PRODUCT_DEFINITION ( 'UNKNOWN', '', #157115, #32847 ) ;
#171352=VECTOR ( 'NONE', #136926, 1000.000000000000000 ) ;
#171452=LINE ( 'NONE', #231399, #173472 ) ;
#171591=CARTESIAN_POINT ( 'NONE',  ( -16.93226657140833069, 9.999543822735571297, -113.0787131109736521 ) ) ;
#171642=ORIENTED_EDGE ( 'NONE', *, *, #232564, .T. ) ;
#171762=CARTESIAN_POINT ( 'NONE',  ( -14.00000000000000178, 9.850000000011133849, -117.2500000000000284 ) ) ;
#172009=DIRECTION ( 'NONE',  ( -1.000000000000000000, -0.000000000000000000, -0.000000000000000000 ) ) ;
#172074=ORIENTED_EDGE ( 'NONE', *, *, #76590, .F. ) ;
#172483=VECTOR ( 'NONE', #93732, 1000.000000000000000 ) ;
#172612=EDGE_CURVE ( 'NONE', #168680, #93005, #136163, .T. ) ;
#173032=CARTESIAN_POINT ( 'NONE',  ( -16.87333278164142314, 9.882609784590052016, -113.6331678061527128 ) ) ;
#173038=CARTESIAN_POINT ( 'NONE',  ( 12.26145404764308644, 9.351413679112543065, -117.4803435675489993 ) ) ;
#173472=VECTOR ( 'NONE', #228830, 1000.000000000000000 ) ;
#173535=CARTESIAN_POINT ( 'NONE',  ( -18.40000000000000213, 11.47316190337364183, -121.4500000000000313 ) ) ;
#173726=CARTESIAN_POINT ( 'NONE',  ( -16.97683809663752186, 9.950000000011138823, -120.5976359818037196 ) ) ;
#173903=ORIENTED_EDGE ( 'NONE', *, *, #102361, .T. ) ;
#174100=CARTESIAN_POINT ( 'NONE',  ( 17.74533788810829904, 10.81849979148195118, -123.6863773250524616 ) ) ;
#174132=CARTESIAN_POINT ( 'NONE',  ( -18.44085059012131822, 11.51401249349495970, -124.7403053191215747 ) ) ;
#174171=VECTOR ( 'NONE', #119992, 1000.000000000000000 ) ;
#174183=ADVANCED_FACE ( 'NONE', ( #49316 ), #94851, .F. ) ;
#174220=CARTESIAN_POINT ( 'NONE',  ( -16.92507428761700439, 9.950000000011138823, -113.2133974596215893 ) ) ;
#174316=CARTESIAN_POINT ( 'NONE',  ( -16.80621392010904103, 9.942202577518958861, -113.1895919654167670 ) ) ;
#174348=DIRECTION ( 'NONE',  ( 1.000000000000000000, 0.000000000000000000, 0.000000000000000000 ) ) ;
#174429=CARTESIAN_POINT ( 'NONE',  ( -17.11825945287481332, 10.05000000001113847, -121.2500000000000426 ) ) ;
#174814=CARTESIAN_POINT ( 'NONE',  ( -16.94389599338512298, 9.991197989766199328, -113.1076448018102809 ) ) ;
#174917=CARTESIAN_POINT ( 'NONE',  ( -16.85939591225058365, 9.905226478398999390, -113.4600682464690777 ) ) ;
#175210=EDGE_CURVE ( 'NONE', #77508, #122635, #74422, .T. ) ;
#175211=LINE ( 'NONE', #136006, #199832 ) ;
#175240=CARTESIAN_POINT ( 'NONE',  ( -18.35668295345803713, 11.47316190337363118, -124.7500000000000426 ) ) ;
#175362=CIRCLE ( 'NONE', #221111, 0.1000000000000001305 ) ;
#175369=CARTESIAN_POINT ( 'NONE',  ( 16.87683809663749557, 9.950000000011131718, -121.3500000000000369 ) ) ;
#175447=ORIENTED_EDGE ( 'NONE', *, *, #175632, .F. ) ;
#175523=FACE_OUTER_BOUND ( 'NONE', #257567, .T. ) ;
#175562=DIRECTION ( 'NONE',  ( -0.000000000000000000, -0.000000000000000000, -1.000000000000000000 ) ) ;
#175605=( LENGTH_UNIT ( ) NAMED_UNIT ( * ) SI_UNIT ( .MILLI., .METRE. ) );
#175616=EDGE_CURVE ( 'NONE', #14870, #107983, #230276, .T. ) ;
#175632=EDGE_CURVE ( 'NONE', #229722, #42531, #205317, .T. ) ;
#175676=DIRECTION ( 'NONE',  ( 0.000000000000000000, 0.000000000000000000, 1.000000000000000000 ) ) ;
#176028=CARTESIAN_POINT ( 'NONE',  ( -18.35235881385853318, 11.47341900772405054, -109.7500000000000426 ) ) ;
#176064=CARTESIAN_POINT ( 'NONE',  ( -16.77779411440718604, 9.946101447118758543, -121.3369425829955048 ) ) ;
#176078=CARTESIAN_POINT ( 'NONE',  ( -16.94333152886235894, 9.990342011461637028, -113.1079684689456286 ) ) ;
#176266=CARTESIAN_POINT ( 'NONE',  ( -16.90138253750127362, 9.950000000011138823, -121.2115627079046618 ) ) ;
#176456=EDGE_CURVE ( 'NONE', #197503, #49384, #52431, .T. ) ;
#176563=CARTESIAN_POINT ( 'NONE',  ( -16.94107738177415712, 10.01423928514777728, -113.0500000000000398 ) ) ;
#176607=PLANE ( 'NONE',  #33266 ) ;
#176654=ORIENTED_EDGE ( 'NONE', *, *, #29598, .F. ) ;
#176821=ORIENTED_EDGE ( 'NONE', *, *, #242167, .F. ) ;
#176847=LINE ( 'NONE', #58132, #48776 ) ;
#176849=CARTESIAN_POINT ( 'NONE',  ( -17.71734398241073549, 10.84235722847571637, -123.7251382530056105 ) ) ;
#176972=ORIENTED_EDGE ( 'NONE', *, *, #97100, .F. ) ;
#177084=AXIS2_PLACEMENT_3D ( 'NONE', #198655, #254733, #96951 ) ;
#177189=ORIENTED_EDGE ( 'NONE', *, *, #113998, .F. ) ;
#177317=B_SPLINE_CURVE_WITH_KNOTS ( 'NONE', 3,
 ( #7226, #106317, #183318, #50203, #185874, #47627, #5933, #245858, #146723, #68508 ),
 .UNSPECIFIED., .F., .F.,
 ( 4, 2, 2, 2, 4 ),
 ( 0.000000000000000000, 0.0003916577441626822214, 0.0005874866162440240368, 0.0006854010522846949987, 0.0007833154883253658522 ),
 .UNSPECIFIED. ) ;
#177764=DIRECTION ( 'NONE',  ( -1.000000000000000000, 3.854941057726231589E-15, 0.000000000000000000 ) ) ;
#177941=FACE_OUTER_BOUND ( 'NONE', #25841, .T. ) ;
#178478=LINE ( 'NONE', #59753, #197263 ) ;
#178539=FILL_AREA_STYLE ('',( #98939 ) ) ;
#178752=CARTESIAN_POINT ( 'NONE',  ( -16.79139129368504157, 9.944944162472831195, -113.1702446328258560 ) ) ;
#178852=CARTESIAN_POINT ( 'NONE',  ( -16.87401514999228525, 9.950000000011137047, -121.2800179925321231 ) ) ;
#179105=ORIENTED_EDGE ( 'NONE', *, *, #26071, .F. ) ;
#179158=MECHANICAL_DESIGN_GEOMETRIC_PRESENTATION_REPRESENTATION('',(#145793),#212646);
#179299=VERTEX_POINT ( 'NONE', #78540 ) ;
#179319=CARTESIAN_POINT ( 'NONE',  ( 23.04999999999999716, 8.822561741677553471, -109.7500000000000426 ) ) ;
#179349=EDGE_LOOP ( 'NONE', ( #94661, #45680, #129982 ) ) ;
#179394=CARTESIAN_POINT ( 'NONE',  ( -16.89268316805465986, 9.951721813253337601, -121.3557524785455826 ) ) ;
#179419=FACE_OUTER_BOUND ( 'NONE', #217425, .T. ) ;
#179494=ORIENTED_EDGE ( 'NONE', *, *, #83882, .T. ) ;
#179615=AXIS2_PLACEMENT_3D ( 'NONE', #250618, #193234, #208936 ) ;
#179670=( BOUNDED_SURFACE ( )  B_SPLINE_SURFACE ( 3, 2, ( 
 ( #85989, #24801, #188979 ),
 ( #63895, #187714, #165578 ),
 ( #48172, #69051, #226812 ),
 ( #183839, #208559, #247666 ) ),
 .UNSPECIFIED., .F., .F., .F. ) 
 B_SPLINE_SURFACE_WITH_KNOTS ( ( 4, 4 ),
 ( 3, 3 ),
 ( 4.712388980384689674, 5.765869716888531116 ),
 ( 0.000000000000000000, 1.000000000000000000 ),
 .UNSPECIFIED. ) 
 GEOMETRIC_REPRESENTATION_ITEM ( )  RATIONAL_B_SPLINE_SURFACE ( (
 ( 1.000000000000000000, 0.7071067811864985009, 1.000000000000000000),
 ( 1.000000000000000000, 0.7953136715912955124, 1.000000000000000000),
 ( 1.000000000000000000, 0.8646876308615905060, 1.000000000000000000),
 ( 1.000000000000000000, 0.8984936768950610997, 1.000000000000000000) ) ) 
 REPRESENTATION_ITEM ( '' )  SURFACE ( )  );
#179701=DIRECTION ( 'NONE',  ( -1.000000000000000000, 0.000000000000000000, 0.000000000000000000 ) ) ;
#179707=ORIENTED_EDGE ( 'NONE', *, *, #97100, .T. ) ;
#179713=CARTESIAN_POINT ( 'NONE',  ( 21.72449340488909897, 10.28395627750227703, -121.3500000000000227 ) ) ;
#180226=VERTEX_POINT ( 'NONE', #143847 ) ;
#180238=CARTESIAN_POINT ( 'NONE',  ( -14.00000000000000178, 9.850000000011133849, -117.2500000000000284 ) ) ;
#180255=DIRECTION ( 'NONE',  ( 1.000000000000000000, 0.000000000000000000, 0.000000000000000000 ) ) ;
#180817=CARTESIAN_POINT ( 'NONE',  ( -16.81931177881023132, 9.936996059515065483, -121.2732178786172597 ) ) ;
#180924=VERTEX_POINT ( 'NONE', #2452 ) ;
#180981=AXIS2_PLACEMENT_3D ( 'NONE', #111191, #190757, #12114 ) ;
#181093=CARTESIAN_POINT ( 'NONE',  ( 23.04999999999999716, 8.822561741677553471, -121.3500000000000227 ) ) ;
#181175=( BOUNDED_CURVE ( )  B_SPLINE_CURVE ( 3, ( #176563, #211831, #93144, #256022 ),
 .UNSPECIFIED., .F., .F. ) 
 B_SPLINE_CURVE_WITH_KNOTS ( ( 4, 4 ),
 ( 0.3000847527772381729, 0.5497968875596814797 ),
 .UNSPECIFIED. ) 
 CURVE ( )  GEOMETRIC_REPRESENTATION_ITEM ( )  RATIONAL_B_SPLINE_CURVE ( ( 1.000000000000000000, 0.9948104011409419911, 0.9948104011409419911, 1.000000000000000000 ) ) 
 REPRESENTATION_ITEM ( '' )  );
#181223=VERTEX_POINT ( 'NONE', #96105 ) ;
#182330=ORIENTED_EDGE ( 'NONE', *, *, #129349, .F. ) ;
#182349=CARTESIAN_POINT ( 'NONE',  ( -18.40000000000000213, 8.822561741677553471, -109.7500000000000426 ) ) ;
#182480=LINE ( 'NONE', #161641, #205590 ) ;
#182542=CARTESIAN_POINT ( 'NONE',  ( 13.99999999999999822, 9.850000000011137402, -117.2500000000000284 ) ) ;
#182655=CARTESIAN_POINT ( 'NONE',  ( -16.97683809663752186, 9.850000000011140955, -113.1500000000000341 ) ) ;
#182686=CARTESIAN_POINT ( 'NONE',  ( -16.89155683852579060, 9.950000000011137047, -120.7226281504603378 ) ) ;
#182712=DIRECTION ( 'NONE',  ( 1.000000000000000000, -0.000000000000000000, -0.000000000000000000 ) ) ;
#182892=CARTESIAN_POINT ( 'NONE',  ( -20.65000000000000568, 7.250000000011138646, -113.1500000000000341 ) ) ;
#182996=ORIENTED_EDGE ( 'NONE', *, *, #56964, .T. ) ;
#183127=EDGE_CURVE ( 'NONE', #14167, #77508, #165485, .T. ) ;
#183223=EDGE_LOOP ( 'NONE', ( #21625, #250338, #3597, #56251 ) ) ;
#183250=ORIENTED_EDGE ( 'NONE', *, *, #183127, .F. ) ;
#183259=ORIENTED_EDGE ( 'NONE', *, *, #252443, .T. ) ;
#183318=CARTESIAN_POINT ( 'NONE',  ( -16.97048326478264713, 9.950000000011137047, -113.6411068801271966 ) ) ;
#183398=ORIENTED_EDGE ( 'NONE', *, *, #91630, .T. ) ;
#183493=DIRECTION ( 'NONE',  ( 0.000000000000000000, 0.000000000000000000, -1.000000000000000000 ) ) ;
#183652=DIRECTION ( 'NONE',  ( 1.000000000000000000, 0.000000000000000000, 0.000000000000000000 ) ) ;
#183701=FACE_OUTER_BOUND ( 'NONE', #4221, .T. ) ;
#183839=CARTESIAN_POINT ( 'NONE',  ( -16.87242674293850087, 9.950000000011138823, -113.1489097536276773 ) ) ;
#184223=CARTESIAN_POINT ( 'NONE',  ( 23.24999999999999645, 8.822561741677553471, -121.3500000000000227 ) ) ;
#185210=LINE ( 'NONE', #62701, #153070 ) ;
#185216=VERTEX_POINT ( 'NONE', #237202 ) ;
#185392=ADVANCED_FACE ( 'NONE', ( #205760 ), #25863, .F. ) ;
#185802=CARTESIAN_POINT ( 'NONE',  ( 12.84233041328155878, 9.410538608540022665, -115.9326879971408886 ) ) ;
#185874=CARTESIAN_POINT ( 'NONE',  ( -16.92989143108098560, 9.950000000011138823, -113.3824838747567298 ) ) ;
#185920=FACE_OUTER_BOUND ( 'NONE', #238698, .T. ) ;
#186084=DIRECTION ( 'NONE',  ( -1.000000000000000000, -0.000000000000000000, -0.000000000000000000 ) ) ;
#186105=DIRECTION ( 'NONE',  ( 0.000000000000000000, 0.000000000000000000, 1.000000000000000000 ) ) ;
#186155=DIRECTION ( 'NONE',  ( 1.000000000000000000, 1.186688945009009831E-16, 0.000000000000000000 ) ) ;
#186197=EDGE_CURVE ( 'NONE', #38363, #45147, #118691, .T. ) ;
#186430=CARTESIAN_POINT ( 'NONE',  ( 20.27550659511088682, 9.216043722520002035, -109.7500000000000426 ) ) ;
#186465=ORIENTED_EDGE ( 'NONE', *, *, #199235, .F. ) ;
#186734=CARTESIAN_POINT ( 'NONE',  ( 18.39999999999999503, 8.822561741677553471, -124.7500000000000284 ) ) ;
#186934=CARTESIAN_POINT ( 'NONE',  ( -14.56556274378147897, 9.446557523083686903, -115.5899419543459175 ) ) ;
#186966=CARTESIAN_POINT ( 'NONE',  ( -15.55912972643741199, 8.490870273573719373, -113.1500000000000341 ) ) ;
#187005=CARTESIAN_POINT ( 'NONE',  ( -18.34374000495059676, 11.47316190337362940, -124.7500000000000426 ) ) ;
#187035=VECTOR ( 'NONE', #187443, 1000.000000000000000 ) ;
#187148=VECTOR ( 'NONE', #240029, 1000.000000000000000 ) ;
#187443=DIRECTION ( 'NONE',  ( 1.000000000000000000, -0.000000000000000000, -0.000000000000000000 ) ) ;
#187472=EDGE_CURVE ( 'NONE', #237169, #146785, #17298, .T. ) ;
#187662=EDGE_CURVE ( 'NONE', #162376, #150801, #120274, .T. ) ;
#187714=CARTESIAN_POINT ( 'NONE',  ( -17.05016517656157404, 9.950000000013014656, -113.1726979960009629 ) ) ;
#187931=CARTESIAN_POINT ( 'NONE',  ( -18.34374000495060386, 11.47316190337362585, -109.7500000000000284 ) ) ;
#188169=PLANE ( 'NONE',  #119366 ) ;
#188194=CARTESIAN_POINT ( 'NONE',  ( -12.25000000000000178, 9.350000000011139178, -117.2500000000000284 ) ) ;
#188282=CARTESIAN_POINT ( 'NONE',  ( -16.77683809663752257, 9.945835743215303282, -121.3360509808958341 ) ) ;
#188416=CARTESIAN_POINT ( 'NONE',  ( -18.40000000000000213, 11.33174054713633261, -121.3500000000000369 ) ) ;
#188509=CARTESIAN_POINT ( 'NONE',  ( -12.48127053791145258, 9.376580978055097049, -118.1269462470119862 ) ) ;
#188710=CARTESIAN_POINT ( 'NONE',  ( 20.27550659511089037, 9.216043722519994930, -121.3500000000000227 ) ) ;
#188943=DIRECTION ( 'NONE',  ( 1.186688945009009831E-16, -1.000000000000000000, 0.000000000000000000 ) ) ;
#188979=CARTESIAN_POINT ( 'NONE',  ( -17.11825945287482753, 10.05000000001113847, -113.1500000000000483 ) ) ;
#189017=VERTEX_POINT ( 'NONE', #154017 ) ;
#189119=CARTESIAN_POINT ( 'NONE',  ( -16.81744102076748959, 9.950000000011138823, -121.3500000000000369 ) ) ;
#189320=CARTESIAN_POINT ( 'NONE',  ( -17.29158576265543346, 10.36474766602906783, -122.5827582447922026 ) ) ;
#189725=CYLINDRICAL_SURFACE ( 'NONE', #216035, 0.9000000000000014655 ) ;
#189773=PLANE ( 'NONE',  #54071 ) ;
#189841=CARTESIAN_POINT ( 'NONE',  ( -18.40000000000000213, 11.48667500176882328, -109.7500000000000426 ) ) ;
#189860=VECTOR ( 'NONE', #207336, 1000.000000000000000 ) ;
#189991=CARTESIAN_POINT ( 'NONE',  ( 14.22916352759893321, 9.457410930301314522, -118.9999159087462886 ) ) ;
#190016=EDGE_LOOP ( 'NONE', ( #213355, #83977, #59310, #22728 ) ) ;
#190229=CARTESIAN_POINT ( 'NONE',  ( 13.99999999999999822, 9.850000000011137402, -117.2500000000000284 ) ) ;
#190757=DIRECTION ( 'NONE',  ( -1.073024830501117725E-15, 0.000000000000000000, 1.000000000000000000 ) ) ;
#191188=ORIENTED_EDGE ( 'NONE', *, *, #164320, .F. ) ;
#191200=PLANE ( 'NONE',  #170893 ) ;
#191485=LINE ( 'NONE', #246296, #212947 ) ;
#191580=DIRECTION ( 'NONE',  ( -0.000000000000000000, -0.000000000000000000, -1.000000000000000000 ) ) ;
#191591=CARTESIAN_POINT ( 'NONE',  ( -18.44085059012131822, 11.51401249349495437, -109.7596946808784963 ) ) ;
#191811=ADVANCED_FACE ( 'NONE', ( #90932 ), #207043, .F. ) ;
#191844=ADVANCED_FACE ( 'NONE', ( #54375 ), #27312, .T. ) ;
#191864=ORIENTED_EDGE ( 'NONE', *, *, #209680, .F. ) ;
#191929=EDGE_CURVE ( 'NONE', #221470, #228853, #124627, .T. ) ;
#192531=AXIS2_PLACEMENT_3D ( 'NONE', #229136, #106591, #186155 ) ;
#192614=CARTESIAN_POINT ( 'NONE',  ( -16.86445178670641809, 9.962211629127180501, -113.1092225618826319 ) ) ;
#192846=DIRECTION ( 'NONE',  ( 1.000000000000000000, 1.186688945009010077E-16, 0.000000000000000000 ) ) ;
#193228=CARTESIAN_POINT ( 'NONE',  ( -23.25000000000000355, 9.950000000011138823, -109.7500000000000426 ) ) ;
#193234=DIRECTION ( 'NONE',  ( -0.000000000000000000, -0.000000000000000000, -1.000000000000000000 ) ) ;
#193243=CARTESIAN_POINT ( 'NONE',  ( -16.86133551771148475, 9.950000000011137047, -121.3013434345467090 ) ) ;
#193303=CARTESIAN_POINT ( 'NONE',  ( -16.90987985657661952, 9.957807518190888274, -121.3692870888836666 ) ) ;
#193371=ORIENTED_EDGE ( 'NONE', *, *, #199194, .T. ) ;
#193413=DIRECTION ( 'NONE',  ( -1.073024830501117725E-15, -0.000000000000000000, -1.000000000000000000 ) ) ;
#193699=CARTESIAN_POINT ( 'NONE',  ( -16.93440969289731513, 9.995185175825110235, -113.0912341850108191 ) ) ;
#193702=B_SPLINE_CURVE_WITH_KNOTS ( 'NONE', 3,
 ( #2490, #20811, #148119, #127269, #108973, #22090, #239848, #82008, #160329, #88104, #140732, #241142, #220292, #8609, #208109, #227639 ),
 .UNSPECIFIED., .F., .F.,
 ( 4, 3, 3, 3, 3, 4 ),
 ( 0.000000000000000000, 1.810570668009715449E-05, 2.740575833571675123E-05, 4.256816319436012815E-05, 5.213463471026095184E-05, 6.641585710718307266E-05 ),
 .UNSPECIFIED. ) ;
#193838=CARTESIAN_POINT ( 'NONE',  ( -16.87683809663752399, 9.850000000011123191, -113.9023640181965220 ) ) ;
#193847=CARTESIAN_POINT ( 'NONE',  ( 12.68104795156993880, 9.396533993965071829, -118.4059397791733090 ) ) ;
#193878=EDGE_CURVE ( 'NONE', #11411, #107983, #45800, .T. ) ;
#193907=CARTESIAN_POINT ( 'NONE',  ( -16.87036670365549895, 9.989418819312803066, -113.0204398826979855 ) ) ;
#193909=CARTESIAN_POINT ( 'NONE',  ( -16.93388492042257454, 9.988541822527057690, -121.4005451231862054 ) ) ;
#194147=CARTESIAN_POINT ( 'NONE',  ( -16.94107738177415357, 10.01423928514777728, -113.0500000000000256 ) ) ;
#194205=EDGE_LOOP ( 'NONE', ( #182330, #247639, #110609, #191188, #23999 ) ) ;
#194384=ORIENTED_EDGE ( 'NONE', *, *, #40055, .F. ) ;
#194549=ADVANCED_FACE ( 'NONE', ( #211508 ), #69444, .T. ) ;
#194783=CARTESIAN_POINT ( 'NONE',  ( -18.34374000495059676, 11.47316190337362940, -124.7500000000000426 ) ) ;
#194904=ORIENTED_EDGE ( 'NONE', *, *, #40055, .T. ) ;
#194962=CARTESIAN_POINT ( 'NONE',  ( 18.39999999999999503, 11.75000000001113953, -124.7500000000000426 ) ) ;
#194996=CARTESIAN_POINT ( 'NONE',  ( -16.93906926870270624, 10.01214687095770906, -113.0534523072268485 ) ) ;
#195597=EDGE_CURVE ( 'NONE', #67859, #41586, #147831, .T. ) ;
#195733=CARTESIAN_POINT ( 'NONE',  ( 15.74999999999999645, 9.350000000011139178, -117.2500000000000284 ) ) ;
#195814=CYLINDRICAL_SURFACE ( 'NONE', #136241, 1.500000000000001332 ) ;
#195919=B_SPLINE_CURVE_WITH_KNOTS ( 'NONE', 3,
 ( #89400, #166416, #145523, #64712, #144229, #227626, #188509, #48995, #223771, #245927, #85523, #244624, #107685, #168991, #149410, #128541, #45148, #165101, #67278, #225047, #228929, #46419, #146795, #205496, #26905, #226326, #47703, #127257, #206795, #56663 ),
 .UNSPECIFIED., .F., .F.,
 ( 4, 2, 2, 2, 2, 2, 2, 2, 2, 2, 2, 2, 2, 2, 4 ),
 ( 0.000000000000000000, 0.0003422764154113355664, 0.0006845528308226711328, 0.001026829246234006862, 0.001369105661645342266, 0.002053658492468009387, 0.002738211323290676725, 0.003080487738702010828, 0.003422764154113344063, 0.003765040569524678166, 0.004107316984936011835, 0.004449593400347345504, 0.004791869815758679173, 0.005134146231170016311, 0.005476422646581353450 ),
 .UNSPECIFIED. ) ;
#196872=CARTESIAN_POINT ( 'NONE',  ( -16.77828822459933633, 9.946229375067616729, -121.3373717490810861 ) ) ;
#196885=CARTESIAN_POINT ( 'NONE',  ( -18.40000000000000213, 5.650000000011139001, -121.3500000000000369 ) ) ;
#196899=LINE ( 'NONE', #75693, #160145 ) ;
#197117=CARTESIAN_POINT ( 'NONE',  ( -17.11825945287481332, 10.05000000001113847, -121.3500000000000369 ) ) ;
#197162=ORIENTED_EDGE ( 'NONE', *, *, #240855, .T. ) ;
#197222=ADVANCED_FACE ( 'NONE', ( #160422 ), #22184, .T. ) ;
#197263=VECTOR ( 'NONE', #136739, 1000.000000000000000 ) ;
#197306=VECTOR ( 'NONE', #66397, 1000.000000000000000 ) ;
#197405=EDGE_CURVE ( 'NONE', #75834, #145735, #130850, .T. ) ;
#197459=CYLINDRICAL_SURFACE ( 'NONE', #150046, 1.749999999999998002 ) ;
#197503=VERTEX_POINT ( 'NONE', #134082 ) ;
#197579=DIRECTION ( 'NONE',  ( -1.000000000000000000, -0.000000000000000000, 1.073024830501117725E-15 ) ) ;
#197617=DIRECTION ( 'NONE',  ( 0.000000000000000000, 0.000000000000000000, 1.000000000000000000 ) ) ;
#197816=ORIENTED_EDGE ( 'NONE', *, *, #126356, .T. ) ;
#197863=CYLINDRICAL_SURFACE ( 'NONE', #257785, 1.749999999999999778 ) ;
#197938=VECTOR ( 'NONE', #211096, 1000.000000000000000 ) ;
#198230=VECTOR ( 'NONE', #209901, 1000.000000000000000 ) ;
#198345=DIRECTION ( 'NONE',  ( -1.000000000000000000, 1.652117596168391700E-15, 0.000000000000000000 ) ) ;
#198374=CARTESIAN_POINT ( 'NONE',  ( -16.82542659449980604, 9.934499891438555608, -121.2553643999738142 ) ) ;
#198463=DIRECTION ( 'NONE',  ( 1.186688945009010077E-16, -1.000000000000000000, -0.000000000000000000 ) ) ;
#198613=EDGE_CURVE ( 'NONE', #162352, #122635, #72785, .T. ) ;
#198655=CARTESIAN_POINT ( 'NONE',  ( 20.04999999999999716, 8.750000000011173285, -121.3500000000000227 ) ) ;
#198771=CARTESIAN_POINT ( 'NONE',  ( -17.22767730082750504, 10.34924421247735182, -122.6424286905667458 ) ) ;
#198914=CARTESIAN_POINT ( 'NONE',  ( -16.87368910959167678, 9.961273816702552963, -113.1124930966406197 ) ) ;
#198919=DIRECTION ( 'NONE',  ( -1.000000000000000000, 0.000000000000000000, 0.000000000000000000 ) ) ;
#199081=DIRECTION ( 'NONE',  ( -0.000000000000000000, -0.000000000000000000, 1.000000000000000000 ) ) ;
#199194=EDGE_CURVE ( 'NONE', #33727, #14870, #137428, .T. ) ;
#199235=EDGE_CURVE ( 'NONE', #180226, #28001, #135620, .T. ) ;
#199262=EDGE_LOOP ( 'NONE', ( #142585, #199444 ) ) ;
#199392=( BOUNDED_CURVE ( )  B_SPLINE_CURVE ( 3, ( #7589, #221480, #145803, #42870 ),
 .UNSPECIFIED., .F., .F. ) 
 B_SPLINE_CURVE_WITH_KNOTS ( ( 4, 4 ),
 ( 1.570796326794885012, 3.141592653589794448 ),
 .UNSPECIFIED. ) 
 CURVE ( )  GEOMETRIC_REPRESENTATION_ITEM ( )  RATIONAL_B_SPLINE_CURVE ( ( 1.000000000000000000, 0.8047378541243619399, 0.8047378541243619399, 1.000000000000000000 ) ) 
 REPRESENTATION_ITEM ( '' )  );
#199444=ORIENTED_EDGE ( 'NONE', *, *, #116054, .T. ) ;
#199523=EDGE_CURVE ( 'NONE', #33727, #37705, #90296, .T. ) ;
#199587=CARTESIAN_POINT ( 'NONE',  ( -16.80100426158789872, 9.943150520407291637, -113.1829457528341010 ) ) ;
#199738=EDGE_CURVE ( 'NONE', #162005, #21871, #219993, .T. ) ;
#199795=DIRECTION ( 'NONE',  ( -1.020425574104004196E-15, -0.000000000000000000, -1.000000000000000000 ) ) ;
#199832=VECTOR ( 'NONE', #215559, 1000.000000000000000 ) ;
#199951=VERTEX_POINT ( 'NONE', #47758 ) ;
#200082=DIRECTION ( 'NONE',  ( 0.000000000000000000, -0.000000000000000000, -1.000000000000000000 ) ) ;
#200201=AXIS2_PLACEMENT_3D ( 'NONE', #115398, #254852, #200082 ) ;
#200267=ORIENTED_EDGE ( 'NONE', *, *, #125615, .T. ) ;
#200572=CARTESIAN_POINT ( 'NONE',  ( 18.39999999999998082, 11.47316190337362585, -109.7500000000000284 ) ) ;
#200735=VERTEX_POINT ( 'NONE', #54542 ) ;
#200785=CIRCLE ( 'NONE', #163379, 0.09999999999999939493 ) ;
#200944=CARTESIAN_POINT ( 'NONE',  ( -16.83558968593875349, 9.950000000011137047, -121.3376948123833188 ) ) ;
#201274=ORIENTED_EDGE ( 'NONE', *, *, #172612, .T. ) ;
#201438=LINE ( 'NONE', #124491, #215607 ) ;
#202156=VECTOR ( 'NONE', #25279, 1000.000000000000000 ) ;
#202169=CARTESIAN_POINT ( 'NONE',  ( -16.77732147278574715, 9.945966932584587639, -113.1635087568758422 ) ) ;
#202520=ADVANCED_FACE ( 'NONE', ( #69794 ), #189725, .F. ) ;
#202797=CARTESIAN_POINT ( 'NONE',  ( 15.39793903038207823, 9.389686005666810331, -116.1728435063513416 ) ) ;
#202822=EDGE_CURVE ( 'NONE', #168103, #89874, #27814, .T. ) ;
#202869=AXIS2_PLACEMENT_3D ( 'NONE', #158164, #236365, #180255 ) ;
#203062=CARTESIAN_POINT ( 'NONE',  ( -23.25000000000000355, 5.650000000011139001, -113.1500000000000341 ) ) ;
#203068=LINE ( 'NONE', #106514, #225345 ) ;
#203146=PLANE ( 'NONE',  #192531 ) ;
#203456=CARTESIAN_POINT ( 'NONE',  ( -16.78569801330232636, 9.947933733124651567, -113.1569129053475393 ) ) ;
#203607=ORIENTED_EDGE ( 'NONE', *, *, #249812, .F. ) ;
#203609=DIRECTION ( 'NONE',  ( -1.000000000000000000, 0.000000000000000000, -1.020425574104004196E-15 ) ) ;
#204105=CARTESIAN_POINT ( 'NONE',  ( -16.89797118371625828, 9.976380722655289190, -121.4372933675582260 ) ) ;
#204141=DIRECTION ( 'NONE',  ( -0.000000000000000000, -0.000000000000000000, -1.000000000000000000 ) ) ;
#204255=ORIENTED_EDGE ( 'NONE', *, *, #114921, .T. ) ;
#204669=FACE_OUTER_BOUND ( 'NONE', #44113, .T. ) ;
#205029=FACE_OUTER_BOUND ( 'NONE', #256414, .T. ) ;
#205196=LINE ( 'NONE', #186966, #25423 ) ;
#205317=B_SPLINE_CURVE_WITH_KNOTS ( 'NONE', 3,
 ( #251079, #110295, #12511, #189841 ),
 .UNSPECIFIED., .F., .F.,
 ( 4, 4 ),
 ( 0.000000000000000000, 7.713889350929433657E-05 ),
 .UNSPECIFIED. ) ;
#205428=CARTESIAN_POINT ( 'NONE',  ( -17.11825945287481687, 9.950000000011138823, -121.2500000000000284 ) ) ;
#205431=ADVANCED_FACE ( 'NONE', ( #41028 ), #117972, .F. ) ;
#205473=DIRECTION ( 'NONE',  ( 0.000000000000000000, 0.000000000000000000, 1.000000000000000000 ) ) ;
#205482=EDGE_CURVE ( 'NONE', #163086, #54629, #205196, .T. ) ;
#205496=CARTESIAN_POINT ( 'NONE',  ( -15.51798037960204368, 9.376659938544690931, -118.1281925482173136 ) ) ;
#205590=VECTOR ( 'NONE', #118662, 1000.000000000000000 ) ;
#205751=DIRECTION ( 'NONE',  ( 1.000000000000000000, 0.000000000000000000, -0.000000000000000000 ) ) ;
#205760=FACE_OUTER_BOUND ( 'NONE', #214439, .T. ) ;
#206139=ORIENTED_EDGE ( 'NONE', *, *, #63267, .F. ) ;
#206210=EDGE_CURVE ( 'NONE', #104724, #110479, #213897, .T. ) ;
#206294=CARTESIAN_POINT ( 'NONE',  ( 15.48841904831874849, 8.561580951692381092, -121.3500000000000369 ) ) ;
#206468=CARTESIAN_POINT ( 'NONE',  ( -15.15766958671844122, 9.410538608540022665, -115.9326879971409312 ) ) ;
#206722=EDGE_LOOP ( 'NONE', ( #129727, #255484, #238804, #153029, #169494, #4817, #216594, #230319, #144841 ) ) ;
#206795=CARTESIAN_POINT ( 'NONE',  ( -15.75000000000001066, 9.350000000011142731, -117.3642676076161706 ) ) ;
#207017=VECTOR ( 'NONE', #104686, 1000.000000000000000 ) ;
#207043=PLANE ( 'NONE',  #253882 ) ;
#207102=EDGE_CURVE ( 'NONE', #233466, #229059, #49730, .T. ) ;
#207336=DIRECTION ( 'NONE',  ( -0.000000000000000000, -0.000000000000000000, -1.000000000000000000 ) ) ;
#207648=VECTOR ( 'NONE', #71563, 1000.000000000000000 ) ;
#207860=ORIENTED_EDGE ( 'NONE', *, *, #29389, .F. ) ;
#207914=DIRECTION ( 'NONE',  ( -1.000000000000000000, -1.186688945009010077E-16, -0.000000000000000000 ) ) ;
#208109=CARTESIAN_POINT ( 'NONE',  ( -16.94132844910801694, 9.992436755191500097, -121.3962017559823607 ) ) ;
#208427=CARTESIAN_POINT ( 'NONE',  ( -18.40000000000000213, 11.33174054713633261, -121.3500000000000369 ) ) ;
#208530=ORIENTED_EDGE ( 'NONE', *, *, #114716, .T. ) ;
#208559=CARTESIAN_POINT ( 'NONE',  ( -16.91049119928364064, 9.950000000011138823, -113.1182796068092102 ) ) ;
#208619=CARTESIAN_POINT ( 'NONE',  ( 22.88900146558018989, 8.703904791123973084, -109.7500000000000426 ) ) ;
#208936=DIRECTION ( 'NONE',  ( -1.000000000000000000, 0.000000000000000000, 0.000000000000000000 ) ) ;
#209042=EDGE_CURVE ( 'NONE', #122635, #104512, #234289, .T. ) ;
#209086=B_SPLINE_CURVE_WITH_KNOTS ( 'NONE', 3,
 ( #7153, #125822, #4583, #144089, #167557, #185802, #86673, #45012, #222331, #244488, #63281, #106244, #104945, #247047, #142798, #243199, #65851, #227488, #224915, #245786, #123265, #202797, #68435, #223625, #67143, #84081 ),
 .UNSPECIFIED., .F., .F.,
 ( 4, 2, 2, 2, 2, 2, 2, 2, 2, 2, 2, 2, 4 ),
 ( 0.005476422646581343041, 0.006160811967703572201, 0.006845201288825802227, 0.007187395949386904230, 0.007529590609948006233, 0.007871785270509109103, 0.008213979931070210239, 0.008556174591631313109, 0.008898369252192414244, 0.009240563912753517115, 0.009582758573314618250, 0.01026714789443682399, 0.01095153721555902800 ),
 .UNSPECIFIED. ) ;
#209540=CARTESIAN_POINT ( 'NONE',  ( -16.87683809663750978, 9.950000000011137047, -113.9023640181965220 ) ) ;
#209591=ORIENTED_EDGE ( 'NONE', *, *, #63131, .T. ) ;
#209604=VERTEX_POINT ( 'NONE', #217942 ) ;
#209680=EDGE_CURVE ( 'NONE', #245594, #163086, #81002, .T. ) ;
#209681=DIRECTION ( 'NONE',  ( 0.000000000000000000, 0.000000000000000000, 1.000000000000000000 ) ) ;
#209785=ORIENTED_EDGE ( 'NONE', *, *, #243745, .F. ) ;
#209901=DIRECTION ( 'NONE',  ( -1.000000000000000000, 0.000000000000000000, -0.000000000000000000 ) ) ;
#210297=CARTESIAN_POINT ( 'NONE',  ( -16.94445028196807002, 9.992063609708893068, -121.3926698215815918 ) ) ;
#210323=EDGE_CURVE ( 'NONE', #45147, #160776, #255902, .T. ) ;
#210498=DIRECTION ( 'NONE',  ( -0.000000000000000000, 1.000000000000000000, -0.000000000000000000 ) ) ;
#210683=CARTESIAN_POINT ( 'NONE',  ( -16.93909480342659890, 9.993078364812696179, -113.1003470166723588 ) ) ;
#210824=CARTESIAN_POINT ( 'NONE',  ( -16.79270642812322478, 9.946244216949072126, -113.1610667214380044 ) ) ;
#210825=EDGE_CURVE ( 'NONE', #15255, #168103, #85194, .T. ) ;
#210925=EDGE_CURVE ( 'NONE', #181223, #44121, #249897, .T. ) ;
#211096=DIRECTION ( 'NONE',  ( 0.000000000000000000, -1.000000000000000000, 0.000000000000000000 ) ) ;
#211298=CIRCLE ( 'NONE', #157151, 14.30833333333333890 ) ;
#211508=FACE_OUTER_BOUND ( 'NONE', #256107, .T. ) ;
#211624=( BOUNDED_CURVE ( )  B_SPLINE_CURVE ( 3, ( #81709, #139118, #161307, #240830 ),
 .UNSPECIFIED., .F., .F. ) 
 B_SPLINE_CURVE_WITH_KNOTS ( ( 4, 4 ),
 ( 4.712388980384689674, 5.672655318024773408 ),
 .UNSPECIFIED. ) 
 CURVE ( )  GEOMETRIC_REPRESENTATION_ITEM ( )  RATIONAL_B_SPLINE_CURVE ( ( 1.000000000000000000, 0.9246222802177227473, 0.9246222802177227473, 1.000000000000000000 ) ) 
 REPRESENTATION_ITEM ( '' )  );
#211664=DIRECTION ( 'NONE',  ( 1.000000000000000000, -0.000000000000000000, -0.000000000000000000 ) ) ;
#211724=CARTESIAN_POINT ( 'NONE',  ( -16.27683809663750480, 9.350000000011133849, -121.4500000000000313 ) ) ;
#211831=CARTESIAN_POINT ( 'NONE',  ( -17.29158576265544056, 10.36474766602906605, -111.9172417552078684 ) ) ;
#212120=CARTESIAN_POINT ( 'NONE',  ( -16.83233564386401682, 9.930221796595743555, -113.2754793365244126 ) ) ;
#212144=FACE_OUTER_BOUND ( 'NONE', #108133, .T. ) ;
#212253=CARTESIAN_POINT ( 'NONE',  ( -16.87372397896795562, 9.880599536652891146, -120.8507245100358176 ) ) ;
#212421=CARTESIAN_POINT ( 'NONE',  ( -17.78241384942104020, 10.85557575279232800, -110.7490376724656187 ) ) ;
#212646=( GEOMETRIC_REPRESENTATION_CONTEXT ( 3 ) GLOBAL_UNCERTAINTY_ASSIGNED_CONTEXT ( ( #44026 ) ) GLOBAL_UNIT_ASSIGNED_CONTEXT ( ( #28463, #224037, #243612 ) ) REPRESENTATION_CONTEXT ( 'NONE', 'WORKASPACE' ) );
#212892=CARTESIAN_POINT ( 'NONE',  ( -13.54795643572457919, 9.450668889178686527, -115.5555464902073766 ) ) ;
#212947=VECTOR ( 'NONE', #53226, 1000.000000000000000 ) ;
#213239=CARTESIAN_POINT ( 'NONE',  ( -16.93255653858138388, 9.998451453988312920, -113.0816433679897131 ) ) ;
#213355=ORIENTED_EDGE ( 'NONE', *, *, #207102, .F. ) ;
#213378=CARTESIAN_POINT ( 'NONE',  ( -16.97683809663752186, 9.950000000011137047, -113.9023640181965220 ) ) ;
#213607=VECTOR ( 'NONE', #5847, 1000.000000000000000 ) ;
#213897=LINE ( 'NONE', #236024, #171352 ) ;
#213990=CARTESIAN_POINT ( 'NONE',  ( -16.81930730667006202, 9.936998068885202429, -113.2267677305382136 ) ) ;
#214081=CARTESIAN_POINT ( 'NONE',  ( -16.97683809663754317, 9.950000000011140600, -120.7284708321106166 ) ) ;
#214173=CARTESIAN_POINT ( 'NONE',  ( -12.84409460144753545, 9.410682294279107296, -115.9311434419482936 ) ) ;
#214439=EDGE_LOOP ( 'NONE', ( #183259, #2258 ) ) ;
#214525=CARTESIAN_POINT ( 'NONE',  ( -16.94445028196808778, 9.992063609708889516, -113.1073301784184792 ) ) ;
#214665=CARTESIAN_POINT ( 'NONE',  ( -16.93710578446423654, 9.950000000011137047, -113.4188039837994353 ) ) ;
#214674=CARTESIAN_POINT ( 'NONE',  ( 14.45963434102924161, 9.451541661396667848, -118.9538754988305840 ) ) ;
#214753=ORIENTED_EDGE ( 'NONE', *, *, #138034, .F. ) ;
#214801=CARTESIAN_POINT ( 'NONE',  ( -20.65000000000000568, 5.650000000011139001, -109.7500000000000426 ) ) ;
#214837=LINE ( 'NONE', #34962, #221465 ) ;
#215137=VECTOR ( 'NONE', #150175, 1000.000000000000000 ) ;
#215248=CARTESIAN_POINT ( 'NONE',  ( -12.25000000000000178, 9.850000000011133849, -117.2500000000000284 ) ) ;
#215341=FACE_OUTER_BOUND ( 'NONE', #243896, .T. ) ;
#215356=CARTESIAN_POINT ( 'NONE',  ( -16.81744102076748959, 9.950000000011138823, -121.3500000000000369 ) ) ;
#215559=DIRECTION ( 'NONE',  ( -1.000000000000000000, 0.000000000000000000, 0.000000000000000000 ) ) ;
#215589=CARTESIAN_POINT ( 'NONE',  ( -18.39418127959864790, 11.48390560170929220, -124.7500000000000284 ) ) ;
#215607=VECTOR ( 'NONE', #103602, 1000.000000000000000 ) ;
#215736=EDGE_CURVE ( 'NONE', #78857, #230044, #6257, .T. ) ;
#215882=DIRECTION ( 'NONE',  ( -0.000000000000000000, -0.000000000000000000, -1.000000000000000000 ) ) ;
#216015=EDGE_LOOP ( 'NONE', ( #21685, #28676, #85273, #173903, #86364, #156707, #21562, #43400, #91385, #78432, #32551, #58656 ) ) ;
#216035=AXIS2_PLACEMENT_3D ( 'NONE', #90602, #170214, #249698 ) ;
#216160=CARTESIAN_POINT ( 'NONE',  ( 13.99999999999999822, 9.850000000011137402, -117.2500000000000284 ) ) ;
#216230=LINE ( 'NONE', #36354, #172483 ) ;
#216421=ORIENTED_EDGE ( 'NONE', *, *, #114152, .F. ) ;
#216582=FACE_OUTER_BOUND ( 'NONE', #206722, .T. ) ;
#216594=ORIENTED_EDGE ( 'NONE', *, *, #1956, .F. ) ;
#216653=FACE_OUTER_BOUND ( 'NONE', #134335, .T. ) ;
#216957=EDGE_CURVE ( 'NONE', #167911, #199951, #178478, .T. ) ;
#217039=CARTESIAN_POINT ( 'NONE',  ( -17.78241384940961112, 10.85557575278324904, -123.7509623275517470 ) ) ;
#217092=CARTESIAN_POINT ( 'NONE',  ( 20.05000000000002913, 7.250000000011171508, -113.1500000000000483 ) ) ;
#217258=FILL_AREA_STYLE ('',( #137727 ) ) ;
#217425=EDGE_LOOP ( 'NONE', ( #209591, #257955, #224565, #171085, #121791, #219624, #101299, #258088, #252803, #162517, #47242, #65517, #95494, #126754, #235628, #51892, #77852, #150688 ) ) ;
#217528=CYLINDRICAL_SURFACE ( 'NONE', #101250, 0.1000000000000028644 ) ;
#217913=CARTESIAN_POINT ( 'NONE',  ( -16.97683810757273193, 9.950000000011137047, -120.7364232875395942 ) ) ;
#217942=CARTESIAN_POINT ( 'NONE',  ( 21.13736287352038445, 8.046642376395153562, -113.1500000000000483 ) ) ;
#218003=EDGE_LOOP ( 'NONE', ( #10414, #76797, #228148, #191864 ) ) ;
#218719=DIRECTION ( 'NONE',  ( 1.186688945009010077E-16, -1.000000000000000000, -0.000000000000000000 ) ) ;
#218813=ORIENTED_EDGE ( 'NONE', *, *, #144012, .F. ) ;
#218967=CARTESIAN_POINT ( 'NONE',  ( -18.34374000495060386, 11.47316190337362585, -109.7500000000000284 ) ) ;
#219012=LINE ( 'NONE', #196885, #123411 ) ;
#219096=ORIENTED_EDGE ( 'NONE', *, *, #79196, .T. ) ;
#219127=CARTESIAN_POINT ( 'NONE',  ( 18.39999999999997371, 11.75000000001113953, -109.7500000000000426 ) ) ;
#219212=CARTESIAN_POINT ( 'NONE',  ( -16.77431908686106254, 9.945805754529134290, -121.3358392176502747 ) ) ;
#219447=EDGE_LOOP ( 'NONE', ( #156451, #164657, #138129, #113528 ) ) ;
#219624=ORIENTED_EDGE ( 'NONE', *, *, #110111, .T. ) ;
#219993=LINE ( 'NONE', #158771, #139561 ) ;
#220162=ORIENTED_EDGE ( 'NONE', *, *, #224707, .T. ) ;
#220187=ORIENTED_EDGE ( 'NONE', *, *, #30834, .F. ) ;
#220292=CARTESIAN_POINT ( 'NONE',  ( -16.93658211146644987, 9.994108662352344297, -121.4042950699557082 ) ) ;
#220347=FACE_OUTER_BOUND ( 'NONE', #194205, .T. ) ;
#220511=ORIENTED_EDGE ( 'NONE', *, *, #91630, .F. ) ;
#220520=CARTESIAN_POINT ( 'NONE',  ( -16.80070461187883879, 9.950000000011266721, -121.3530361708397010 ) ) ;
#220623=CARTESIAN_POINT ( 'NONE',  ( -18.40000000000000213, 11.75000000001113953, -113.1500000000000341 ) ) ;
#220641=DIRECTION ( 'NONE',  ( 1.186688945009009831E-16, -1.000000000000000000, 0.000000000000000000 ) ) ;
#220796=( BOUNDED_CURVE ( )  B_SPLINE_CURVE ( 3, ( #200572, #221395, #138013, #38948 ),
 .UNSPECIFIED., .F., .F. ) 
 B_SPLINE_CURVE_WITH_KNOTS ( ( 4, 4 ),
 ( 2.589852378279005940, 2.850972632318389710 ),
 .UNSPECIFIED. ) 
 CURVE ( )  GEOMETRIC_REPRESENTATION_ITEM ( )  RATIONAL_B_SPLINE_CURVE ( ( 1.000000000000000000, 0.9943260843901262636, 0.9943260843901262636, 1.000000000000000000 ) ) 
 REPRESENTATION_ITEM ( '' )  );
#220861=ORIENTED_EDGE ( 'NONE', *, *, #101765, .F. ) ;
#220928=AXIS2_PLACEMENT_3D ( 'NONE', #8906, #247516, #147116 ) ;
#221111=AXIS2_PLACEMENT_3D ( 'NONE', #228013, #169364, #48083 ) ;
#221122=EDGE_LOOP ( 'NONE', ( #71014, #135450, #12397, #107289, #249620, #110115, #29299, #44569, #111422, #23216 ) ) ;
#221156=VERTEX_POINT ( 'NONE', #145576 ) ;
#221395=CARTESIAN_POINT ( 'NONE',  ( 17.74533788810830615, 10.81849979148195118, -110.8136226749475952 ) ) ;
#221465=VECTOR ( 'NONE', #114459, 1000.000000000000000 ) ;
#221470=VERTEX_POINT ( 'NONE', #217092 ) ;
#221480=CARTESIAN_POINT ( 'NONE',  ( -18.40000000000000213, 11.41458325961093756, -113.1500000000000483 ) ) ;
#221702=CARTESIAN_POINT ( 'NONE',  ( -16.77779411503079032, 9.946101446935278645, -113.1630574176198678 ) ) ;
#221734=CARTESIAN_POINT ( 'NONE',  ( -21.64999999999999858, 10.05000000001113847, -121.2500000000000426 ) ) ;
#221765=EDGE_CURVE ( 'NONE', #14167, #104512, #159110, .T. ) ;
#222160=EDGE_CURVE ( 'NONE', #209604, #112606, #250180, .T. ) ;
#222179=DIRECTION ( 'NONE',  ( -0.7071067811865463515, 0.7071067811865487940, -0.000000000000000000 ) ) ;
#222331=CARTESIAN_POINT ( 'NONE',  ( 13.22261339317536333, 9.436552840015579591, -115.6779554727603312 ) ) ;
#222463=CARTESIAN_POINT ( 'NONE',  ( 20.27550659511089037, 9.216043722520002035, -121.3500000000000227 ) ) ;
#222531=PLANE ( 'NONE',  #84909 ) ;
#222613=EDGE_CURVE ( 'NONE', #37705, #37503, #254189, .T. ) ;
#222747=CARTESIAN_POINT ( 'NONE',  ( -16.87683809663752399, 21.23804903844422043, -113.1500000000000341 ) ) ;
#222809=EDGE_CURVE ( 'NONE', #221156, #41586, #201438, .T. ) ;
#222886=PLANE ( 'NONE',  #143132 ) ;
#222959=DIRECTION ( 'NONE',  ( -1.000000000000000000, 0.000000000000000000, 0.000000000000000000 ) ) ;
#223040=FACE_OUTER_BOUND ( 'NONE', #25460, .T. ) ;
#223179=CARTESIAN_POINT ( 'NONE',  ( -20.65000000000000568, 7.250000000011138646, -113.1500000000000341 ) ) ;
#223202=CARTESIAN_POINT ( 'NONE',  ( 16.87683809663749557, 9.950000000011131718, -121.3500000000000369 ) ) ;
#223346=EDGE_CURVE ( 'NONE', #42531, #180924, #158809, .T. ) ;
#223445=CARTESIAN_POINT ( 'NONE',  ( -15.70407651835961005, 9.355806591641286474, -116.7911025315462012 ) ) ;
#223625=CARTESIAN_POINT ( 'NONE',  ( 15.70340296795547808, 9.355888454513701546, -116.7886428967780574 ) ) ;
#223697=CARTESIAN_POINT ( 'NONE',  ( -16.88853107394619357, 9.950878483358135185, -121.3529363468922639 ) ) ;
#223711=VECTOR ( 'NONE', #87068, 1000.000000000000000 ) ;
#223771=CARTESIAN_POINT ( 'NONE',  ( -12.68215100488889924, 9.396630376328870327, -118.4070573928183023 ) ) ;
#224027=DIRECTION ( 'NONE',  ( 0.000000000000000000, 0.000000000000000000, -1.000000000000000000 ) ) ;
#224037=( NAMED_UNIT ( * ) PLANE_ANGLE_UNIT ( ) SI_UNIT ( $, .RADIAN. ) );
#224106=PLANE ( 'NONE',  #142435 ) ;
#224295=EDGE_CURVE ( 'NONE', #106745, #71546, #138325, .T. ) ;
#224565=ORIENTED_EDGE ( 'NONE', *, *, #256324, .T. ) ;
#224707=EDGE_CURVE ( 'NONE', #228258, #80890, #61066, .T. ) ;
#224906=ADVANCED_FACE ( 'NONE', ( #11376 ), #92182, .F. ) ;
#224915=CARTESIAN_POINT ( 'NONE',  ( 14.87567385445977308, 9.430764995433477793, -115.7305373947504989 ) ) ;
#225047=CARTESIAN_POINT ( 'NONE',  ( -15.06720934482788188, 9.417690691074263043, -118.6416006967646695 ) ) ;
#225171=ORIENTED_EDGE ( 'NONE', *, *, #244882, .F. ) ;
#225180=AXIS2_PLACEMENT_3D ( 'NONE', #47907, #247391, #11366 ) ;
#225255=ORIENTED_EDGE ( 'NONE', *, *, #1956, .T. ) ;
#225345=VECTOR ( 'NONE', #186084, 1000.000000000000000 ) ;
#225463=LINE ( 'NONE', #248913, #143597 ) ;
#225470=CARTESIAN_POINT ( 'NONE',  ( -16.97683809663752186, 9.850000000011137402, -113.9023640181965220 ) ) ;
#225927=CARTESIAN_POINT ( 'NONE',  ( 18.39999999999999503, 11.75000000001113953, -121.3500000000000369 ) ) ;
#226099=ORIENTED_EDGE ( 'NONE', *, *, #210323, .F. ) ;
#226253=CARTESIAN_POINT ( 'NONE',  ( -16.89146115310546037, 9.951443245667611848, -121.3548224189542424 ) ) ;
#226269=AXIS2_PLACEMENT_3D ( 'NONE', #252826, #75511, #155057 ) ;
#226326=CARTESIAN_POINT ( 'NONE',  ( -15.66061380678752535, 9.360723793997191677, -117.8139271946067481 ) ) ;
#226462=( BOUNDED_CURVE ( )  B_SPLINE_CURVE ( 3, ( #187931, #25022, #104501, #87516 ),
 .UNSPECIFIED., .F., .F. ) 
 B_SPLINE_CURVE_WITH_KNOTS ( ( 4, 4 ),
 ( 5.731445031868799056, 5.983100554402348337 ),
 .UNSPECIFIED. ) 
 CURVE ( )  GEOMETRIC_REPRESENTATION_ITEM ( )  RATIONAL_B_SPLINE_CURVE ( ( 1.000000000000000000, 0.9947294176030464508, 0.9947294176030464508, 1.000000000000000000 ) ) 
 REPRESENTATION_ITEM ( '' )  );
#226812=CARTESIAN_POINT ( 'NONE',  ( -16.97092634996651483, 10.00088896635950420, -113.1301427662976948 ) ) ;
#227488=CARTESIAN_POINT ( 'NONE',  ( 14.77516762759922031, 9.436674251854007878, -115.6768619309992516 ) ) ;
#227560=ORIENTED_EDGE ( 'NONE', *, *, #114921, .F. ) ;
#227626=CARTESIAN_POINT ( 'NONE',  ( -12.42749937872396337, 9.370689921613768902, -118.0264651266610656 ) ) ;
#227639=CARTESIAN_POINT ( 'NONE',  ( -16.94445028196807002, 9.992063609708893068, -121.3926698215815918 ) ) ;
#227834=PLANE ( 'NONE',  #225180 ) ;
#227892=PLANE ( 'NONE',  #101440 ) ;
#227904=ORIENTED_EDGE ( 'NONE', *, *, #195597, .F. ) ;
#227967=CARTESIAN_POINT ( 'NONE',  ( -18.40000000000000213, 11.47316190337364183, -121.4500000000000313 ) ) ;
#228009=EDGE_CURVE ( 'NONE', #105539, #45147, #159527, .T. ) ;
#228013=CARTESIAN_POINT ( 'NONE',  ( -16.87036670365549895, 10.08494996326643189, -113.0500000000000398 ) ) ;
#228014=CARTESIAN_POINT ( 'NONE',  ( -16.89268316805466341, 9.951721813253341153, -113.1442475214544885 ) ) ;
#228092=PLANE ( 'NONE',  #238514 ) ;
#228148=ORIENTED_EDGE ( 'NONE', *, *, #13775, .F. ) ;
#228153=EDGE_CURVE ( 'NONE', #137732, #157238, #112388, .T. ) ;
#228258=VERTEX_POINT ( 'NONE', #157641 ) ;
#228259=ORIENTED_EDGE ( 'NONE', *, *, #206210, .T. ) ;
#228266=ORIENTED_EDGE ( 'NONE', *, *, #112045, .F. ) ;
#228830=DIRECTION ( 'NONE',  ( -0.000000000000000000, -0.000000000000000000, -1.000000000000000000 ) ) ;
#228853=VERTEX_POINT ( 'NONE', #104971 ) ;
#228929=CARTESIAN_POINT ( 'NONE',  ( -15.15564720441980739, 9.410708747058238899, -118.5692084058441793 ) ) ;
#229059=VERTEX_POINT ( 'NONE', #120460 ) ;
#229116=CARTESIAN_POINT ( 'NONE',  ( 13.22461703343585171, 9.436662931810239741, -118.8230367322948950 ) ) ;
#229136=CARTESIAN_POINT ( 'NONE',  ( -14.00000000000000178, 9.850000000011133849, -117.2500000000000284 ) ) ;
#229143=EDGE_CURVE ( 'NONE', #180924, #15255, #240378, .T. ) ;
#229579=ORIENTED_EDGE ( 'NONE', *, *, #114716, .F. ) ;
#229722=VERTEX_POINT ( 'NONE', #32622 ) ;
#229816=DIRECTION ( 'NONE',  ( -0.7071067811865456854, 0.7071067811865493491, 0.000000000000000000 ) ) ;
#229829=CARTESIAN_POINT ( 'NONE',  ( 15.48841904831874849, 8.561580951692381092, -113.1500000000000341 ) ) ;
#230044=VERTEX_POINT ( 'NONE', #119843 ) ;
#230243=CARTESIAN_POINT ( 'NONE',  ( -16.93262454970420094, 10.00202046794151300, -113.0729237737627244 ) ) ;
#230276=B_SPLINE_CURVE_WITH_KNOTS ( 'NONE', 3,
 ( #214525, #134971, #114144, #35922, #210683, #32075, #129850, #193699, #111591, #213239, #171591, #71195, #230243, #115427, #75060, #194996, #132436, #249819, #34641 ),
 .UNSPECIFIED., .F., .F.,
 ( 4, 3, 3, 3, 3, 3, 4 ),
 ( 0.0001624081864585820618, 0.0001685232196531672496, 0.0001764526673566887201, 0.0001916878551483116016, 0.0002009890782182490127, 0.0002238845907555078393, 0.0002283406619926233426 ),
 .UNSPECIFIED. ) ;
#230319=ORIENTED_EDGE ( 'NONE', *, *, #91439, .F. ) ;
#230387=CARTESIAN_POINT ( 'NONE',  ( -16.97683810757273193, 9.950000000011137047, -113.7635767124605621 ) ) ;
#230396=CARTESIAN_POINT ( 'NONE',  ( 13.54577453029516043, 9.450602096099677496, -118.9438959630967076 ) ) ;
#230518=EDGE_CURVE ( 'NONE', #167911, #185216, #53333, .T. ) ;
#230609=ORIENTED_EDGE ( 'NONE', *, *, #222809, .F. ) ;
#230713=ORIENTED_EDGE ( 'NONE', *, *, #141163, .F. ) ;
#230749=CARTESIAN_POINT ( 'NONE',  ( -21.65000000000000213, 10.05000000001113847, -121.3500000000000369 ) ) ;
#230972=ADVANCED_FACE ( 'NONE', ( #215341 ), #195814, .T. ) ;
#230980=DIRECTION ( 'NONE',  ( -0.000000000000000000, 1.000000000000000000, -0.000000000000000000 ) ) ;
#231034=EDGE_CURVE ( 'NONE', #52458, #199951, #185210, .T. ) ;
#231055=VECTOR ( 'NONE', #74584, 999.9999999999998863 ) ;
#231100=CARTESIAN_POINT ( 'NONE',  ( -16.97048361161166952, 9.950000000011135270, -120.8588843444304217 ) ) ;
#231234=DIRECTION ( 'NONE',  ( 1.186688945009010077E-16, -1.000000000000000000, -0.000000000000000000 ) ) ;
#231245=DIRECTION ( 'NONE',  ( 0.000000000000000000, 1.000000000000000000, -0.000000000000000000 ) ) ;
#231345=ORIENTED_EDGE ( 'NONE', *, *, #159749, .F. ) ;
#231399=CARTESIAN_POINT ( 'NONE',  ( -20.65000000000000568, 7.250000000011138646, -109.7500000000000426 ) ) ;
#231590=DIRECTION ( 'NONE',  ( 1.000000000000000000, 0.000000000000000000, 0.000000000000000000 ) ) ;
#231687=CARTESIAN_POINT ( 'NONE',  ( -16.83558968593864336, 9.950000000011137047, -113.1623051876165249 ) ) ;
#231699=CARTESIAN_POINT ( 'NONE',  ( 12.33938619321247998, 9.360723793997191677, -117.8139271946067907 ) ) ;
#231984=CARTESIAN_POINT ( 'NONE',  ( -21.64999999999999858, 10.05000000001113847, -113.2500000000000284 ) ) ;
#232564=EDGE_CURVE ( 'NONE', #54629, #11411, #199392, .T. ) ;
#232610=DIRECTION ( 'NONE',  ( 1.000000000000000000, 0.000000000000000000, -0.000000000000000000 ) ) ;
#232986=( BOUNDED_CURVE ( )  B_SPLINE_CURVE ( 3, ( #175369, #93222, #174100, #153243 ),
 .UNSPECIFIED., .F., .F. ) 
 B_SPLINE_CURVE_WITH_KNOTS ( ( 4, 4 ),
 ( 3.432212674861197410, 3.693332928900581624 ),
 .UNSPECIFIED. ) 
 CURVE ( )  GEOMETRIC_REPRESENTATION_ITEM ( )  RATIONAL_B_SPLINE_CURVE ( ( 1.000000000000000000, 0.9943260843901261525, 0.9943260843901261525, 1.000000000000000000 ) ) 
 REPRESENTATION_ITEM ( '' )  );
#232987=CARTESIAN_POINT ( 'NONE',  ( 13.12229106158773284, 9.430637101707896264, -118.7682606180609923 ) ) ;
#233123=ADVANCED_FACE ( 'NONE', ( #116647 ), #197459, .F. ) ;
#233466=VERTEX_POINT ( 'NONE', #62483 ) ;
#233639=EDGE_CURVE ( 'NONE', #125547, #105539, #127788, .T. ) ;
#233747=CARTESIAN_POINT ( 'NONE',  ( -13.88555196119803803, 9.457431528860068326, -115.4999169378996839 ) ) ;
#233771=AXIS2_PLACEMENT_3D ( 'NONE', #225470, #46837, #84658 ) ;
#233938=VECTOR ( 'NONE', #161406, 1000.000000000000000 ) ;
#233970=ORIENTED_EDGE ( 'NONE', *, *, #199523, .F. ) ;
#234231=EDGE_LOOP ( 'NONE', ( #179105, #151035, #112876, #249244 ) ) ;
#234289=LINE ( 'NONE', #251283, #89352 ) ;
#234290=CARTESIAN_POINT ( 'NONE',  ( -16.94878442675512531, 9.991729103002157331, -113.1117804243621663 ) ) ;
#234294=CARTESIAN_POINT ( 'NONE',  ( -16.95709691156173449, 9.950000000011208101, -121.3399424374903219 ) ) ;
#234465=AXIS2_PLACEMENT_3D ( 'NONE', #157247, #120688, #197617 ) ;
#234497=CARTESIAN_POINT ( 'NONE',  ( -14.00000000000000178, 9.850000000011133849, -117.2500000000000284 ) ) ;
#234604=ORIENTED_EDGE ( 'NONE', *, *, #149417, .F. ) ;
#234811=LINE ( 'NONE', #215248, #256270 ) ;
#234909=EDGE_LOOP ( 'NONE', ( #134498, #66574, #59521, #95661, #200267, #29882 ) ) ;
#235155=LINE ( 'NONE', #252132, #10102 ) ;
#235628=ORIENTED_EDGE ( 'NONE', *, *, #83515, .T. ) ;
#235636=CARTESIAN_POINT ( 'NONE',  ( -16.79140778683509794, 9.944941598865719712, -121.3297372337708282 ) ) ;
#235760=ADVANCED_FACE ( 'NONE', ( #46853 ), #228092, .F. ) ;
#235763=AXIS2_PLACEMENT_3D ( 'NONE', #181093, #127523, #183652 ) ;
#235858=CARTESIAN_POINT ( 'NONE',  ( 18.54999999999999716, 9.950000000011153034, -113.1499999999999773 ) ) ;
#235992=ORIENTED_EDGE ( 'NONE', *, *, #232564, .F. ) ;
#236024=CARTESIAN_POINT ( 'NONE',  ( 23.24999999999999645, 5.650000000011139001, -121.3500000000000227 ) ) ;
#236112=CARTESIAN_POINT ( 'NONE',  ( -16.77683809663752257, 9.945835743215301505, -113.1639490191042512 ) ) ;
#236147=DIRECTION ( 'NONE',  ( -1.000000000000000000, 0.000000000000000000, 0.000000000000000000 ) ) ;
#236209=ORIENTED_EDGE ( 'NONE', *, *, #253395, .T. ) ;
#236365=DIRECTION ( 'NONE',  ( 1.073024830501117725E-15, -0.000000000000000000, -1.000000000000000000 ) ) ;
#236870=CARTESIAN_POINT ( 'NONE',  ( 20.09999999999999787, 9.750000000011137757, -113.1500000000000483 ) ) ;
#236970=DIRECTION ( 'NONE',  ( 0.7071067811865474617, 0.7071067811865474617, 0.000000000000000000 ) ) ;
#237062=CARTESIAN_POINT ( 'NONE',  ( 18.39999999999999503, 11.75000000001113953, -113.1500000000000341 ) ) ;
#237169=VERTEX_POINT ( 'NONE', #179713 ) ;
#237202=CARTESIAN_POINT ( 'NONE',  ( -18.40000000000000213, 11.47316190337364183, -124.6740539331920843 ) ) ;
#237514=CARTESIAN_POINT ( 'NONE',  ( -16.85697194749126027, 9.908543714134777858, -121.0649957323862367 ) ) ;
#237659=EDGE_LOOP ( 'NONE', ( #147372, #83248, #230609, #225255 ) ) ;
#237777=EDGE_CURVE ( 'NONE', #179299, #83901, #209086, .T. ) ;
#237904=FACE_OUTER_BOUND ( 'NONE', #46206, .T. ) ;
#238022=CIRCLE ( 'NONE', #233771, 0.09999999999999939493 ) ;
#238099=ADVANCED_FACE ( 'NONE', ( #237904 ), #102609, .T. ) ;
#238190=LINE ( 'NONE', #119562, #17647 ) ;
#238514=AXIS2_PLACEMENT_3D ( 'NONE', #143405, #144675, #67722 ) ;
#238571=CARTESIAN_POINT ( 'NONE',  ( -16.78270389226384296, 9.947372616628161524, -121.3412070369114986 ) ) ;
#238623=CARTESIAN_POINT ( 'NONE',  ( 18.54999999999999716, 8.750000000011182166, -109.7500000000000426 ) ) ;
#238642=ADVANCED_FACE ( 'NONE', ( #103203 ), #161938, .F. ) ;
#238682=CARTESIAN_POINT ( 'NONE',  ( -16.87683809663752399, 9.850000000011144508, -113.9023640181963373 ) ) ;
#238698=EDGE_LOOP ( 'NONE', ( #186465, #8166, #69556, #152572 ) ) ;
#238763=DIRECTION ( 'NONE',  ( 0.000000000000000000, 0.000000000000000000, -1.000000000000000000 ) ) ;
#238795=CARTESIAN_POINT ( 'NONE',  ( -16.92280123533709357, 9.950000000011137047, -121.1493676859149531 ) ) ;
#238804=ORIENTED_EDGE ( 'NONE', *, *, #205482, .T. ) ;
#238974=VECTOR ( 'NONE', #30579, 1000.000000000000000 ) ;
#239011=CARTESIAN_POINT ( 'NONE',  ( 21.72449340488910252, 10.28395627750227703, -113.1500000000000483 ) ) ;
#239221=ORIENTED_EDGE ( 'NONE', *, *, #209042, .F. ) ;
#239273=FACE_OUTER_BOUND ( 'NONE', #7400, .T. ) ;
#239352=CARTESIAN_POINT ( 'NONE',  ( -16.87036670365548474, 9.989418819312801290, -121.4795601173020856 ) ) ;
#239480=CARTESIAN_POINT ( 'NONE',  ( -16.87036670365549895, 9.989418819312803066, -113.0204398826979855 ) ) ;
#239744=ORIENTED_EDGE ( 'NONE', *, *, #257486, .F. ) ;
#239848=CARTESIAN_POINT ( 'NONE',  ( -16.93262454970419384, 10.00202046794151478, -121.4270762262373466 ) ) ;
#240018=CARTESIAN_POINT ( 'NONE',  ( -16.81095280782811230, 9.950000000011138823, -113.1499999999991672 ) ) ;
#240029=DIRECTION ( 'NONE',  ( -0.000000000000000000, 1.000000000000000000, -0.000000000000000000 ) ) ;
#240081=CARTESIAN_POINT ( 'NONE',  ( -16.80621392010910498, 9.942202577518919782, -121.3104080345830909 ) ) ;
#240378=LINE ( 'NONE', #141271, #27808 ) ;
#240708=DIRECTION ( 'NONE',  ( -1.186688945009010077E-16, 1.000000000000000000, 0.000000000000000000 ) ) ;
#240720=ORIENTED_EDGE ( 'NONE', *, *, #224295, .F. ) ;
#240787=CARTESIAN_POINT ( 'NONE',  ( -16.77683809663752257, 9.945835743215303282, -121.3360509808958341 ) ) ;
#240830=CARTESIAN_POINT ( 'NONE',  ( -16.94445028196808778, 9.992063609708889516, -113.1073301784184792 ) ) ;
#240853=DIRECTION ( 'NONE',  ( 1.652117596168391700E-15, 1.000000000000000000, -0.000000000000000000 ) ) ;
#240855=EDGE_CURVE ( 'NONE', #71546, #245454, #158495, .T. ) ;
#241048=CARTESIAN_POINT ( 'NONE',  ( -21.65000000000000213, 7.250000000011138646, -121.3500000000000369 ) ) ;
#241119=CYLINDRICAL_SURFACE ( 'NONE', #108381, 0.1000000000000028644 ) ;
#241142=CARTESIAN_POINT ( 'NONE',  ( -16.93521499325732549, 9.994786119814678571, -121.4071085410935780 ) ) ;
#241776=ORIENTED_EDGE ( 'NONE', *, *, #113169, .F. ) ;
#242052=ORIENTED_EDGE ( 'NONE', *, *, #223346, .T. ) ;
#242167=EDGE_CURVE ( 'NONE', #180924, #78889, #226462, .T. ) ;
#242370=DIRECTION ( 'NONE',  ( -1.000000000000000000, 0.000000000000000000, 0.000000000000000000 ) ) ;
#242656=CIRCLE ( 'NONE', #42746, 0.09999999999999939493 ) ;
#243199=CARTESIAN_POINT ( 'NONE',  ( 14.45204356427541548, 9.450668889178684751, -115.5555464902073766 ) ) ;
#243224=( BOUNDED_CURVE ( )  B_SPLINE_CURVE ( 3, ( #53867, #113831, #12195, #87824 ),
 .UNSPECIFIED., .F., .F. ) 
 B_SPLINE_CURVE_WITH_KNOTS ( ( 4, 4 ),
 ( 1.570796326794908992, 2.617993877991549034 ),
 .UNSPECIFIED. ) 
 CURVE ( )  GEOMETRIC_REPRESENTATION_ITEM ( )  RATIONAL_B_SPLINE_CURVE ( ( 1.000000000000000000, 0.9106836025229521070, 0.9106836025229521070, 1.000000000000000000 ) ) 
 REPRESENTATION_ITEM ( '' )  );
#243482=CARTESIAN_POINT ( 'NONE',  ( -18.40000000000000213, 11.75000000001113953, -121.3500000000000369 ) ) ;
#243603=CARTESIAN_POINT ( 'NONE',  ( -16.27683809663750480, 9.350000000011133849, -109.7500000000000426 ) ) ;
#243612=( NAMED_UNIT ( * ) SI_UNIT ( $, .STERADIAN. ) SOLID_ANGLE_UNIT ( ) );
#243745=EDGE_CURVE ( 'NONE', #46173, #133581, #238022, .T. ) ;
#243896=EDGE_LOOP ( 'NONE', ( #155720, #194904, #79886, #35829 ) ) ;
#244074=DIRECTION ( 'NONE',  ( 0.000000000000000000, 0.000000000000000000, 1.000000000000000000 ) ) ;
#244168=DIRECTION ( 'NONE',  ( 0.7071067811865456854, -0.7071067811865493491, -0.000000000000000000 ) ) ;
#244354=ORIENTED_EDGE ( 'NONE', *, *, #17346, .F. ) ;
#244488=CARTESIAN_POINT ( 'NONE',  ( 13.43443725621853169, 9.446557523083692232, -115.5899419543459459 ) ) ;
#244553=CARTESIAN_POINT ( 'NONE',  ( -16.87331047859649757, 9.950000000011138823, -121.3500000000000369 ) ) ;
#244624=CARTESIAN_POINT ( 'NONE',  ( -13.54036565897074773, 9.451541661396667848, -118.9538754988306266 ) ) ;
#244882=EDGE_CURVE ( 'NONE', #256969, #160776, #235155, .T. ) ;
#245006=CARTESIAN_POINT ( 'NONE',  ( 18.54999999999999716, 8.750000000011182166, -113.1500000000000341 ) ) ;
#245431=ADVANCED_FACE ( 'NONE', ( #17906 ), #14087, .F. ) ;
#245454=VERTEX_POINT ( 'NONE', #252663 ) ;
#245594=VERTEX_POINT ( 'NONE', #35539 ) ;
#245760=ORIENTED_EDGE ( 'NONE', *, *, #148349, .F. ) ;
#245786=CARTESIAN_POINT ( 'NONE',  ( 15.06592377766031632, 9.417789466963361278, -115.8573845439769059 ) ) ;
#245798=EDGE_LOOP ( 'NONE', ( #124847, #183250, #194384, #155722, #229579, #73801, #244354, #107063, #239744, #148813, #69387, #197162, #177189, #117523 ) ) ;
#245858=CARTESIAN_POINT ( 'NONE',  ( -16.86132326855785735, 9.950000000011135270, -113.1986357846683688 ) ) ;
#245927=CARTESIAN_POINT ( 'NONE',  ( -12.92414019175886253, 9.417632963117446465, -118.6489484657322606 ) ) ;
#246296=CARTESIAN_POINT ( 'NONE',  ( -23.25000000000000355, 5.650000000011139001, -109.7500000000000426 ) ) ;
#246314=CARTESIAN_POINT ( 'NONE',  ( -21.65000000000000213, 9.950000000011140600, -113.2500000000000284 ) ) ;
#246556=DIRECTION ( 'NONE',  ( 0.7071067811865463515, -0.7071067811865487940, 4.930380657631324879E-32 ) ) ;
#246738=CARTESIAN_POINT ( 'NONE',  ( -23.25000000000000355, 5.650000000011139001, -113.1500000000000341 ) ) ;
#246823=CARTESIAN_POINT ( 'NONE',  ( -18.40000000000000213, 11.48667500176882861, -124.7500000000000284 ) ) ;
#246840=DIRECTION ( 'NONE',  ( -1.073024830501117725E-15, 0.000000000000000000, -1.000000000000000000 ) ) ;
#246850=CARTESIAN_POINT ( 'NONE',  ( -18.40000000000000213, 11.33174054713631662, -113.1500000000000341 ) ) ;
#246864=CARTESIAN_POINT ( 'NONE',  ( -14.11697426661281263, 9.457410944778569473, -115.5000839737900833 ) ) ;
#246915=ORIENTED_EDGE ( 'NONE', *, *, #129978, .F. ) ;
#246958=CIRCLE ( 'NONE', #226269, 1.749999999999998002 ) ;
#247010=CARTESIAN_POINT ( 'NONE',  ( -16.81744102076749314, 9.950000000011142376, -113.1500000000000341 ) ) ;
#247047=CARTESIAN_POINT ( 'NONE',  ( 14.11444803880197263, 9.457431528860070102, -115.4999169378997408 ) ) ;
#247078=CARTESIAN_POINT ( 'NONE',  ( -16.92778301347296832, 10.00094491684660092, -121.4285181079681877 ) ) ;
#247200=VECTOR ( 'NONE', #182712, 1000.000000000000000 ) ;
#247349=CARTESIAN_POINT ( 'NONE',  ( 18.39999999999999503, 11.75000000001113953, -124.7500000000000426 ) ) ;
#247370=CARTESIAN_POINT ( 'NONE',  ( -21.65000000000000213, 9.950000000011140600, -121.2500000000000426 ) ) ;
#247391=DIRECTION ( 'NONE',  ( -0.8049926720990042694, -0.5932847527679310229, 0.000000000000000000 ) ) ;
#247516=DIRECTION ( 'NONE',  ( 0.7071067811865487940, 0.7071067811865462405, -7.215498431451186046E-16 ) ) ;
#247573=CARTESIAN_POINT ( 'NONE',  ( -16.87487986503753845, 9.950007555096753720, -113.1499747396867690 ) ) ;
#247639=ORIENTED_EDGE ( 'NONE', *, *, #148349, .T. ) ;
#247666=CARTESIAN_POINT ( 'NONE',  ( -16.93388492042258520, 9.988541822527057690, -113.0994548768138657 ) ) ;
#247754=ORIENTED_EDGE ( 'NONE', *, *, #137237, .F. ) ;
#247982=ORIENTED_EDGE ( 'NONE', *, *, #210825, .T. ) ;
#248027=DIRECTION ( 'NONE',  ( 0.8049926720990051576, 0.5932847527679298016, -0.000000000000000000 ) ) ;
#248164=CARTESIAN_POINT ( 'NONE',  ( -13.43673303185028800, 9.446648990640014176, -115.5891632959231998 ) ) ;
#248234=ORIENTED_EDGE ( 'NONE', *, *, #198613, .F. ) ;
#248265=LINE ( 'NONE', #211724, #134768 ) ;
#248328=ORIENTED_EDGE ( 'NONE', *, *, #17346, .T. ) ;
#248665=CARTESIAN_POINT ( 'NONE',  ( -16.82055514392378726, 9.950000000011137047, -113.1767980745418356 ) ) ;
#248679=CARTESIAN_POINT ( 'NONE',  ( 15.69410316191958898, 9.356746017089403011, -117.7033597213642082 ) ) ;
#248913=CARTESIAN_POINT ( 'NONE',  ( -18.40000000000000213, 11.47316190337362762, -113.1500000000000341 ) ) ;
#248979=CARTESIAN_POINT ( 'NONE',  ( -16.87036670365549540, 9.989418819312804843, -113.0204398826979713 ) ) ;
#249244=ORIENTED_EDGE ( 'NONE', *, *, #210925, .F. ) ;
#249395=ORIENTED_EDGE ( 'NONE', *, *, #186197, .F. ) ;
#249463=CARTESIAN_POINT ( 'NONE',  ( -12.60206096961791999, 9.389686005666813884, -116.1728435063513700 ) ) ;
#249504=LINE ( 'NONE', #252056, #92905 ) ;
#249565=ORIENTED_EDGE ( 'NONE', *, *, #237777, .T. ) ;
#249620=ORIENTED_EDGE ( 'NONE', *, *, #244882, .T. ) ;
#249698=DIRECTION ( 'NONE',  ( -1.000000000000000000, 0.000000000000000000, 0.000000000000000000 ) ) ;
#249812=EDGE_CURVE ( 'NONE', #160776, #197503, #243224, .T. ) ;
#249819=CARTESIAN_POINT ( 'NONE',  ( -16.94037747912386394, 10.01353938249748765, -113.0511309579755306 ) ) ;
#249897=B_SPLINE_CURVE_WITH_KNOTS ( 'NONE', 3,
 ( #64393, #47373, #223445, #128221, #126934, #206468, #27866, #124373, #82628, #186934, #87780, #167370, #246864, #233747, #72107, #212892, #248164, #69544, #150358, #55066, #214173, #249463, #35561, #149081, #134606, #188194 ),
 .UNSPECIFIED., .F., .F.,
 ( 4, 2, 2, 2, 2, 2, 2, 2, 2, 2, 2, 2, 4 ),
 ( 0.005476422646581353450, 0.006160811967703588680, 0.006845201288825822176, 0.007187395949386924179, 0.007529590609948026182, 0.007871785270509128185, 0.008213979931070231055, 0.008556174591631333926, 0.008898369252192435061, 0.009240563912753536197, 0.009582758573314639067, 0.01026714789443684134, 0.01095153721555904534 ),
 .UNSPECIFIED. ) ;
#249962=CARTESIAN_POINT ( 'NONE',  ( 12.48201962039796520, 9.376659938544690931, -118.1281925482173421 ) ) ;
#249987=DIRECTION ( 'NONE',  ( 1.186688945009010077E-16, -1.000000000000000000, -0.000000000000000000 ) ) ;
#250096=CARTESIAN_POINT ( 'NONE',  ( -16.87683809663752399, 9.850000000011144508, -120.5976359818037338 ) ) ;
#250160=ADVANCED_FACE ( 'NONE', ( #148819 ), #10586, .F. ) ;
#250180=LINE ( 'NONE', #154953, #207648 ) ;
#250210=ORIENTED_EDGE ( 'NONE', *, *, #154159, .T. ) ;
#250338=ORIENTED_EDGE ( 'NONE', *, *, #197405, .F. ) ;
#250482=DIRECTION ( 'NONE',  ( 0.000000000000000000, 0.000000000000000000, -1.000000000000000000 ) ) ;
#250524=VERTEX_POINT ( 'NONE', #246314 ) ;
#250618=CARTESIAN_POINT ( 'NONE',  ( 20.73486653747088937, 7.750000000011182166, -109.7500000000000426 ) ) ;
#250919=CARTESIAN_POINT ( 'NONE',  ( -18.40000000000000213, 11.75000000001113953, -121.3500000000000369 ) ) ;
#251079=CARTESIAN_POINT ( 'NONE',  ( -18.39999999999999858, 11.47316190337362762, -109.8259460668080152 ) ) ;
#251084=ORIENTED_EDGE ( 'NONE', *, *, #6035, .T. ) ;
#251188=( BOUNDED_CURVE ( )  B_SPLINE_CURVE ( 3, ( #94053, #32851, #189320, #148916 ),
 .UNSPECIFIED., .F., .F. ) 
 B_SPLINE_CURVE_WITH_KNOTS ( ( 4, 4 ),
 ( 5.733388419619901200, 5.983100554402348337 ),
 .UNSPECIFIED. ) 
 CURVE ( )  GEOMETRIC_REPRESENTATION_ITEM ( )  RATIONAL_B_SPLINE_CURVE ( ( 1.000000000000000000, 0.9948104011409416580, 0.9948104011409416580, 1.000000000000000000 ) ) 
 REPRESENTATION_ITEM ( '' )  );
#251283=CARTESIAN_POINT ( 'NONE',  ( 18.54999999999999716, 8.750000000011182166, -121.3500000000000369 ) ) ;
#251315=VECTOR ( 'NONE', #92458, 1000.000000000000000 ) ;
#251467=AXIS2_PLACEMENT_3D ( 'NONE', #190229, #188943, #126392 ) ;
#251613=VECTOR ( 'NONE', #72319, 1000.000000000000000 ) ;
#251733=CARTESIAN_POINT ( 'NONE',  ( -16.92925196614875816, 9.972331796421277872, -113.1167448477168307 ) ) ;
#252056=CARTESIAN_POINT ( 'NONE',  ( 15.74999999999999645, 9.850000000011137402, -117.2500000000000284 ) ) ;
#252077=CARTESIAN_POINT ( 'NONE',  ( -16.94107738177414291, 10.01423928514777373, -121.4500000000000313 ) ) ;
#252132=CARTESIAN_POINT ( 'NONE',  ( -17.01825945287481545, 9.950000000011138823, -121.2500000000000426 ) ) ;
#252228=( GEOMETRIC_REPRESENTATION_CONTEXT ( 3 ) GLOBAL_UNCERTAINTY_ASSIGNED_CONTEXT ( ( #26992 ) ) GLOBAL_UNIT_ASSIGNED_CONTEXT ( ( #34825, #253825, #37381 ) ) REPRESENTATION_CONTEXT ( 'NONE', 'WORKASPACE' ) );
#252237=DIRECTION ( 'NONE',  ( 0.000000000000000000, 0.000000000000000000, -1.000000000000000000 ) ) ;
#252443=EDGE_CURVE ( 'NONE', #19091, #133581, #131281, .T. ) ;
#252500=CARTESIAN_POINT ( 'NONE',  ( -16.89155683852533230, 9.950000000011138823, -113.7773718495397617 ) ) ;
#252663=CARTESIAN_POINT ( 'NONE',  ( 18.39999999999999503, 11.75000000001113953, -113.1500000000000341 ) ) ;
#252803=ORIENTED_EDGE ( 'NONE', *, *, #30461, .T. ) ;
#252826=CARTESIAN_POINT ( 'NONE',  ( 13.99999999999999822, 9.850000000011137402, -117.2500000000000284 ) ) ;
#252973=EDGE_CURVE ( 'NONE', #180226, #135449, #86992, .T. ) ;
#253395=EDGE_CURVE ( 'NONE', #26064, #209604, #132263, .T. ) ;
#253539=FACE_OUTER_BOUND ( 'NONE', #190016, .T. ) ;
#253576=EDGE_CURVE ( 'NONE', #104512, #228853, #102019, .T. ) ;
#253603=CARTESIAN_POINT ( 'NONE',  ( -18.41431012584569160, 11.48747202921933130, -124.7732360131017231 ) ) ;
#253700=CARTESIAN_POINT ( 'NONE',  ( -17.01473183483381391, 9.950000000011138823, -113.2500000000000426 ) ) ;
#253779=CARTESIAN_POINT ( 'NONE',  ( -16.80070461187914788, 9.950000000011138823, -113.1469638291613649 ) ) ;
#253792=CARTESIAN_POINT ( 'NONE',  ( 13.88638282980484639, 9.457426452500058645, -119.0000418684000749 ) ) ;
#253825=( NAMED_UNIT ( * ) PLANE_ANGLE_UNIT ( ) SI_UNIT ( $, .RADIAN. ) );
#253882=AXIS2_PLACEMENT_3D ( 'NONE', #28444, #107936, #131346 ) ;
#254152=LINE ( 'NONE', #182349, #148650 ) ;
#254189=( BOUNDED_CURVE ( )  B_SPLINE_CURVE ( 3, ( #94629, #174220, #253700, #154645 ),
 .UNSPECIFIED., .F., .F. ) 
 B_SPLINE_CURVE_WITH_KNOTS ( ( 4, 4 ),
 ( 0.5235987755982449698, 1.570796326794896558 ),
 .UNSPECIFIED. ) 
 CURVE ( )  GEOMETRIC_REPRESENTATION_ITEM ( )  RATIONAL_B_SPLINE_CURVE ( ( 1.000000000000000000, 0.9106836025229499976, 0.9106836025229499976, 1.000000000000000000 ) ) 
 REPRESENTATION_ITEM ( '' )  );
#254266=CARTESIAN_POINT ( 'NONE',  ( -16.80117486205003630, 9.949657268323468529, -121.3488548729255143 ) ) ;
#254367=CARTESIAN_POINT ( 'NONE',  ( -16.87683809663752754, 9.864913778549569301, -113.7757156356385480 ) ) ;
#254733=DIRECTION ( 'NONE',  ( -1.073024830501117725E-15, 0.000000000000000000, 1.000000000000000000 ) ) ;
#254760=EDGE_CURVE ( 'NONE', #228853, #229059, #86417, .T. ) ;
#254852=DIRECTION ( 'NONE',  ( 0.000000000000000000, -1.000000000000000000, 0.000000000000000000 ) ) ;
#255151=CARTESIAN_POINT ( 'NONE',  ( -16.87683809663752754, 9.864913447291343118, -120.7242815513040455 ) ) ;
#255388=ORIENTED_EDGE ( 'NONE', *, *, #141163, .T. ) ;
#255484=ORIENTED_EDGE ( 'NONE', *, *, #209680, .T. ) ;
#255514=CARTESIAN_POINT ( 'NONE',  ( -16.80939487329394666, 9.950000000011138823, -121.3500000000009180 ) ) ;
#255527=CARTESIAN_POINT ( 'NONE',  ( -16.93658623642901873, 9.980381671668284937, -113.1119027291292269 ) ) ;
#255711=CARTESIAN_POINT ( 'NONE',  ( 20.04999999999999716, 8.750000000011173285, -109.7500000000000426 ) ) ;
#255902=CIRCLE ( 'NONE', #105894, 0.1000000000000028644 ) ;
#255957=CARTESIAN_POINT ( 'NONE',  ( -18.38817693311004575, 11.48149151591092476, -124.7500000000000284 ) ) ;
#256022=CARTESIAN_POINT ( 'NONE',  ( -18.39999999999999858, 11.47316190337362762, -109.8259460668080152 ) ) ;
#256059=DIRECTION ( 'NONE',  ( -1.646408749285562691E-14, 1.000000000000000000, 0.000000000000000000 ) ) ;
#256107=EDGE_LOOP ( 'NONE', ( #65455, #208530, #27390, #138908 ) ) ;
#256268=CARTESIAN_POINT ( 'NONE',  ( -16.87786941232800686, 9.958154714156124854, -121.3771857997940486 ) ) ;
#256270=VECTOR ( 'NONE', #54868, 1000.000000000000000 ) ;
#256324=EDGE_CURVE ( 'NONE', #37705, #138239, #72943, .T. ) ;
#256414=EDGE_LOOP ( 'NONE', ( #88693, #128792, #15869, #84135 ) ) ;
#256422=CARTESIAN_POINT ( 'NONE',  ( -16.83199318825828783, 9.930646127992318384, -121.2275851882092184 ) ) ;
#256522=CARTESIAN_POINT ( 'NONE',  ( -17.11825945287482753, 10.05000000001113847, -113.1500000000000341 ) ) ;
#256533=ADVANCED_FACE ( 'NONE', ( #3620 ), #217528, .T. ) ;
#256968=ORIENTED_EDGE ( 'NONE', *, *, #252973, .F. ) ;
#256969=VERTEX_POINT ( 'NONE', #247370 ) ;
#256976=VECTOR ( 'NONE', #145123, 1000.000000000000000 ) ;
#257314=ADVANCED_FACE ( 'NONE', ( #179419, #731, #80265 ), #159859, .T. ) ;
#257401=PLANE ( 'NONE',  #44971 ) ;
#257486=EDGE_CURVE ( 'NONE', #200735, #75516, #18416, .T. ) ;
#257567=EDGE_LOOP ( 'NONE', ( #15728, #240720, #85035, #228259 ) ) ;
#257628=EDGE_LOOP ( 'NONE', ( #136268, #104985, #220187, #23907 ) ) ;
#257785=AXIS2_PLACEMENT_3D ( 'NONE', #19234, #93641, #134038 ) ;
#257806=ORIENTED_EDGE ( 'NONE', *, *, #175210, .T. ) ;
#257869=VECTOR ( 'NONE', #55484, 1000.000000000000000 ) ;
#257955=ORIENTED_EDGE ( 'NONE', *, *, #199523, .T. ) ;
#257991=SURFACE_STYLE_FILL_AREA ( #178539 ) ;
#258085=CARTESIAN_POINT ( 'NONE',  ( -16.81744102076748959, 9.950000000011138823, -121.3500000000000369 ) ) ;
#258088=ORIENTED_EDGE ( 'NONE', *, *, #176456, .T. ) ;
ENDSEC;
END-ISO-10303-21;
